ISO-10303-21;
HEADER;
FILE_DESCRIPTION (('STEP AP214'),
    '1' );
FILE_NAME ('circlip for shafts normal_din_Circlip DIN 471 - 8 x 0.8.step',
    '2026-09-28T15:49:00',
    ( '' ),
    ( '' ),
    'SwSTEP 2.0',
    'SolidWorks 2026',
    '' );
FILE_SCHEMA (( 'AUTOMOTIVE_DESIGN' ));
ENDSEC;

DATA;
#36=DIRECTION ( 'NONE',  ( -1.174092375852890260E-15, 4.222049128630259891E-16, 1.000000000000000000 ) ) ;
#79=SURFACE_STYLE_USAGE ( .BOTH. , #8342 ) ;
#105=CARTESIAN_POINT ( 'NONE',  ( 0.1085714285714300953, -3.798448662927791819, -0.7999999999999951594 ) ) ;
#110=CARTESIAN_POINT ( 'NONE',  ( 0.000000000000000000, 0.000000000000000000, -0.7999999999999951594 ) ) ;
#111=DIRECTION ( 'NONE',  ( -1.174092375852890260E-15, 4.222049128630259891E-16, 1.000000000000000000 ) ) ;
#125=FACE_OUTER_BOUND ( 'NONE', #23551, .T. ) ;
#154=EDGE_CURVE ( 'NONE', #9833, #15465, #27896, .T. ) ;
#182=PRESENTATION_STYLE_ASSIGNMENT (( #24683 ) ) ;
#231=EDGE_CURVE ( 'NONE', #22807, #14329, #9992, .T. ) ;
#281=DIRECTION ( 'NONE',  ( 1.000000000000000000, -4.524158825347490025E-15, -1.177133787269970298E-15 ) ) ;
#285=VECTOR ( 'NONE', #5532, 1000.000000000000000 ) ;
#318=ORIENTED_EDGE ( 'NONE', *, *, #12144, .F. ) ;
#418=AXIS2_PLACEMENT_3D ( 'NONE', #11952, #782, #607 ) ;
#420=LINE ( 'NONE', #771, #15850 ) ;
#584=VERTEX_POINT ( 'NONE', #3327 ) ;
#607=DIRECTION ( 'NONE',  ( 1.000000000000000000, -4.528031003192420052E-15, -1.179290629824070178E-15 ) ) ;
#626=FACE_OUTER_BOUND ( 'NONE', #28757, .T. ) ;
#673=FACE_OUTER_BOUND ( 'NONE', #23003, .T. ) ;
#735=PLANE ( 'NONE',  #27972 ) ;
#771=CARTESIAN_POINT ( 'NONE',  ( -1.000000000000014655, -4.808326913196006913, -0.7999999999999951594 ) ) ;
#777=DIRECTION ( 'NONE',  ( 1.000000000000000000, -4.524158825347490025E-15, -1.177133787269970298E-15 ) ) ;
#782=DIRECTION ( 'NONE',  ( -1.174092375852890260E-15, 4.222049128630259891E-16, 1.000000000000000000 ) ) ;
#796=ORIENTED_EDGE ( 'NONE', *, *, #22416, .F. ) ;
#839=ORIENTED_EDGE ( 'NONE', *, *, #27989, .F. ) ;
#879=ORIENTED_EDGE ( 'NONE', *, *, #34561, .T. ) ;
#898=VECTOR ( 'NONE', #11588, 1000.000000000000000 ) ;
#899=LINE ( 'NONE', #25581, #1043 ) ;
#938=EDGE_CURVE ( 'NONE', #16466, #28118, #27417, .T. ) ;
#972=AXIS2_PLACEMENT_3D ( 'NONE', #19881, #17368, #9454 ) ;
#981=DIRECTION ( 'NONE',  ( -1.174092375852890260E-15, 4.222049128630259891E-16, 1.000000000000000000 ) ) ;
#993=CARTESIAN_POINT ( 'NONE',  ( 0.1374368770859640820, -4.808326913196061980, -0.7999999999999951594 ) ) ;
#1043=VECTOR ( 'NONE', #27752, 1000.000000000000000 ) ;
#1046=VECTOR ( 'NONE', #5866, 1000.000000000000000 ) ;
#1060=DIRECTION ( 'NONE',  ( -1.174092375852890260E-15, 4.222049128630259891E-16, 1.000000000000000000 ) ) ;
#1070=CARTESIAN_POINT ( 'NONE',  ( -0.1085714285714300953, -3.798448662927791819, -0.7999999999999951594 ) ) ;
#1197=DIRECTION ( 'NONE',  ( -1.174092375852890260E-15, 4.222049128630259891E-16, 1.000000000000000000 ) ) ;
#1204=ORIENTED_EDGE ( 'NONE', *, *, #28400, .T. ) ;
#1245=ORIENTED_EDGE ( 'NONE', *, *, #9446, .F. ) ;
#1283=MECHANICAL_DESIGN_GEOMETRIC_PRESENTATION_REPRESENTATION('',(#34058),#23722);
#1309=VECTOR ( 'NONE', #7772, 1000.000000000000000 ) ;
#1311=FACE_OUTER_BOUND ( 'NONE', #20645, .T. ) ;
#1359=DIRECTION ( 'NONE',  ( -1.174092375852890260E-15, 4.222049128630259891E-16, 1.000000000000000000 ) ) ;
#1401=CARTESIAN_POINT ( 'NONE',  ( 0.1085714285714300953, -3.798448662927791819, 0.000000000000000000 ) ) ;
#1526=LINE ( 'NONE', #15540, #12639 ) ;
#1574=LINE ( 'NONE', #12367, #20622 ) ;
#1584=FACE_OUTER_BOUND ( 'NONE', #20540, .T. ) ;
#1598=CIRCLE ( 'NONE', #24017, 0.7500000000000039968 ) ;
#1630=EDGE_CURVE ( 'NONE', #13647, #34789, #11717, .T. ) ;
#1765=VECTOR ( 'NONE', #7342, 1000.000000000000000 ) ;
#1862=FACE_OUTER_BOUND ( 'NONE', #34954, .T. ) ;
#1920=AXIS2_PLACEMENT_3D ( 'NONE', #6427, #20269, #30568 ) ;
#1940=CIRCLE ( 'NONE', #1920, 2.447112362156710574 ) ;
#1968=CARTESIAN_POINT ( 'NONE',  ( 0.9999999999999870104, -5.408326913195881325, -0.7999999999999951594 ) ) ;
#1989=CARTESIAN_POINT ( 'NONE',  ( -0.1085714285714300953, -3.798448662927791819, -0.7999999999999951594 ) ) ;
#1991=AXIS2_PLACEMENT_3D ( 'NONE', #12118, #6888, #7062 ) ;
#2005=SHAPE_REPRESENTATION ( 'circlip for shafts normal_din_Circlip DIN 471 - 8 x 0.8', ( #21307 ), #12197 ) ;
#2010=EDGE_LOOP ( 'NONE', ( #15652, #9423, #26123, #30004 ) ) ;
#2014=LINE ( 'NONE', #15484, #3866 ) ;
#2040=VECTOR ( 'NONE', #8936, 1000.000000000000000 ) ;
#2144=AXIS2_PLACEMENT_3D ( 'NONE', #8926, #2852, #6060 ) ;
#2190=DIRECTION ( 'NONE',  ( 1.000000000000000000, -4.524158825347490025E-15, -1.174092375852883357E-15 ) ) ;
#2235=LINE ( 'NONE', #24354, #1309 ) ;
#2239=ADVANCED_BREP_SHAPE_REPRESENTATION ( '', ( #22718, #21307 ), #12197 ) ;
#2312=CARTESIAN_POINT ( 'NONE',  ( 2.141980652367342586, -6.189445006155629869, 0.000000000000000000 ) ) ;
#2336=PRODUCT_DEFINITION_FORMATION_WITH_SPECIFIED_SOURCE ( 'ANY', '', #29075, .NOT_KNOWN. ) ;
#2361=CARTESIAN_POINT ( 'NONE',  ( 0.000000000000000000, 0.000000000000000000, -0.7999999999999951594 ) ) ;
#2393=CARTESIAN_POINT ( 'NONE',  ( -1.387778780781445676E-14, 0.4273491293403097746, 0.000000000000000000 ) ) ;
#2478=CARTESIAN_POINT ( 'NONE',  ( 1.566204647097418912, -6.822536405429468154, -0.7999999999999951594 ) ) ;
#2479=CARTESIAN_POINT ( 'NONE',  ( -1.387778780781445676E-14, 0.4273491293403097746, -0.7999999999999951594 ) ) ;
#2489=DIRECTION ( 'NONE',  ( 0.02857142857142376188, 0.9995917534020517525, 3.884870526907702978E-16 ) ) ;
#2535=CARTESIAN_POINT ( 'NONE',  ( 0.9999999999999870104, -5.408326913195881325, 0.000000000000000000 ) ) ;
#2619=FILL_AREA_STYLE_COLOUR ( '', #3610 ) ;
#2695=DIRECTION ( 'NONE',  ( 1.174092375852890260E-15, -4.222049128630259891E-16, -1.000000000000000000 ) ) ;
#2750=DIRECTION ( 'NONE',  ( -1.174092375852890260E-15, 4.222049128630259891E-16, 1.000000000000000000 ) ) ;
#2763=ORIENTED_EDGE ( 'NONE', *, *, #23606, .T. ) ;
#2819=CARTESIAN_POINT ( 'NONE',  ( 1.599999999999986766, -5.408326913195883989, 7.044554255117328346E-16 ) ) ;
#2852=DIRECTION ( 'NONE',  ( 1.174092375852890260E-15, -4.222049128630259891E-16, -1.000000000000000000 ) ) ;
#2873=CARTESIAN_POINT ( 'NONE',  ( -1.000000000000014655, -4.808326913196006913, -0.7999999999999951594 ) ) ;
#2952=EDGE_LOOP ( 'NONE', ( #28785, #26177, #20547, #21737 ) ) ;
#2984=CARTESIAN_POINT ( 'NONE',  ( 0.1717365941144993746, -6.008326913195982222, 0.000000000000000000 ) ) ;
#3012=STYLED_ITEM ( 'NONE', ( #182 ), #2239 ) ;
#3021=VERTEX_POINT ( 'NONE', #9766 ) ;
#3027=CIRCLE ( 'NONE', #7599, 7.000000000000035527 ) ;
#3028=VERTEX_POINT ( 'NONE', #17497 ) ;
#3175=CYLINDRICAL_SURFACE ( 'NONE', #25301, 0.6000000000000029754 ) ;
#3200=APPLICATION_CONTEXT ( 'automotive_design' ) ;
#3221=DIRECTION ( 'NONE',  ( 1.000000000000000000, -4.607758420995284547E-15, -1.196244974681468202E-15 ) ) ;
#3230=DIRECTION ( 'NONE',  ( 1.174092375852890260E-15, -4.222049128630259891E-16, -1.000000000000000000 ) ) ;
#3296=ORIENTED_EDGE ( 'NONE', *, *, #12144, .T. ) ;
#3327=CARTESIAN_POINT ( 'NONE',  ( -0.2000000000000612399, -6.997142273814382030, -0.7999999999999951594 ) ) ;
#3333=DIRECTION ( 'NONE',  ( 1.174092375852890457E-15, -4.222049128630259891E-16, -1.000000000000000000 ) ) ;
#3356=VECTOR ( 'NONE', #5930, 999.9999999999998863 ) ;
#3378=EDGE_CURVE ( 'NONE', #17419, #26106, #24867, .T. ) ;
#3403=DIRECTION ( 'NONE',  ( 0.02857142857143298714, -0.9995917534020514195, -4.555780455966493806E-16 ) ) ;
#3436=SHAPE_REPRESENTATION_RELATIONSHIP ( 'NONE' , 'NONE' ,  #2005, #2239 ) ;
#3447=DIRECTION ( 'NONE',  ( 1.174092375852890260E-15, -4.222049128630259891E-16, -1.000000000000000000 ) ) ;
#3464=LINE ( 'NONE', #5804, #27125 ) ;
#3466=ORIENTED_EDGE ( 'NONE', *, *, #21355, .F. ) ;
#3528=FACE_OUTER_BOUND ( 'NONE', #11822, .T. ) ;
#3562=CARTESIAN_POINT ( 'NONE',  ( -1.000000000000014655, -4.808326913196006913, -0.7999999999999951594 ) ) ;
#3606=EDGE_CURVE ( 'NONE', #20267, #34652, #31328, .T. ) ;
#3610=COLOUR_RGB ( '', 0.72549020, 0.75294118, 0.79215686) ;
#3645=DIRECTION ( 'NONE',  ( -1.174092375852890260E-15, 4.222049128630259891E-16, 1.000000000000000000 ) ) ;
#3739=AXIS2_PLACEMENT_3D ( 'NONE', #20237, #31247, #17544 ) ;
#3802=CARTESIAN_POINT ( 'NONE',  ( 2.321707774797385326, -4.824281976788927118, -0.7999999999999951594 ) ) ;
#3848=VECTOR ( 'NONE', #15769, 1000.000000000000000 ) ;
#3866=VECTOR ( 'NONE', #21425, 1000.000000000000000 ) ;
#3960=ORIENTED_EDGE ( 'NONE', *, *, #22376, .F. ) ;
#3962=FACE_OUTER_BOUND ( 'NONE', #29901, .T. ) ;
#3975=ORIENTED_EDGE ( 'NONE', *, *, #21561, .T. ) ;
#3988=DIRECTION ( 'NONE',  ( 0.1305261922200477154, 0.9914448613738109373, 2.653430841701508438E-16 ) ) ;
#4010=LINE ( 'NONE', #23061, #19935 ) ;
#4053=CARTESIAN_POINT ( 'NONE',  ( 1.398397006337009918, -6.091550361990587525, -0.7999999999999951594 ) ) ;
#4085=CARTESIAN_POINT ( 'NONE',  ( 2.321707774797385326, -4.824281976788927118, -0.7999999999999951594 ) ) ;
#4089=CYLINDRICAL_SURFACE ( 'NONE', #34332, 7.000000000000035527 ) ;
#4112=DIRECTION ( 'NONE',  ( 1.174092375852890260E-15, -4.222049128630259891E-16, -1.000000000000000000 ) ) ;
#4154=FACE_OUTER_BOUND ( 'NONE', #29496, .T. ) ;
#4188=AXIS2_PLACEMENT_3D ( 'NONE', #2479, #21713, #7674 ) ;
#4210=CARTESIAN_POINT ( 'NONE',  ( 0.1085714285714300953, -3.798448662927791819, -0.7999999999999951594 ) ) ;
#4258=CARTESIAN_POINT ( 'NONE',  ( 0.000000000000000000, 0.000000000000000000, 0.000000000000000000 ) ) ;
#4287=ORIENTED_EDGE ( 'NONE', *, *, #6451, .T. ) ;
#4329=DIRECTION ( 'NONE',  ( -1.174092375852890457E-15, 4.222049128630259891E-16, 1.000000000000000000 ) ) ;
#4397=CYLINDRICAL_SURFACE ( 'NONE', #5550, 3.800000000000018918 ) ;
#4413=ORIENTED_EDGE ( 'NONE', *, *, #14504, .T. ) ;
#4433=CARTESIAN_POINT ( 'NONE',  ( -4.872650870659766653, 0.4273491293403325897, -5.720942237434546063E-15 ) ) ;
#4469=FACE_OUTER_BOUND ( 'NONE', #35133, .T. ) ;
#4511=CIRCLE ( 'NONE', #25777, 2.447112362156710574 ) ;
#4575=ORIENTED_EDGE ( 'NONE', *, *, #21635, .T. ) ;
#4597=ORIENTED_EDGE ( 'NONE', *, *, #7502, .T. ) ;
#4638=VECTOR ( 'NONE', #16706, 1000.000000000000000 ) ;
#4643=VECTOR ( 'NONE', #14961, 1000.000000000000000 ) ;
#4707=CARTESIAN_POINT ( 'NONE',  ( -1.398397006337051440, -6.091550361990532458, 0.000000000000000000 ) ) ;
#4734=CIRCLE ( 'NONE', #19090, 0.7500000000000039968 ) ;
#4872=DIRECTION ( 'NONE',  ( 1.174092375852890260E-15, -4.222049128630259891E-16, -1.000000000000000000 ) ) ;
#4922=LINE ( 'NONE', #21623, #8484 ) ;
#5008=LINE ( 'NONE', #32362, #33147 ) ;
#5178=EDGE_CURVE ( 'NONE', #18718, #18057, #8259, .T. ) ;
#5179=VECTOR ( 'NONE', #10667, 1000.000000000000000 ) ;
#5236=ORIENTED_EDGE ( 'NONE', *, *, #33283, .F. ) ;
#5252=ORIENTED_EDGE ( 'NONE', *, *, #29758, .T. ) ;
#5288=CARTESIAN_POINT ( 'NONE',  ( -3.160591952521663028, -3.281206521718052382, 0.000000000000000000 ) ) ;
#5291=ORIENTED_EDGE ( 'NONE', *, *, #5443, .T. ) ;
#5342=ORIENTED_EDGE ( 'NONE', *, *, #17563, .T. ) ;
#5374=CARTESIAN_POINT ( 'NONE',  ( 0.000000000000000000, 0.000000000000000000, -0.7999999999999951594 ) ) ;
#5409=CARTESIAN_POINT ( 'NONE',  ( -0.1374368770859779598, -4.808326913195978491, 0.000000000000000000 ) ) ;
#5443=EDGE_CURVE ( 'NONE', #18320, #18718, #17590, .T. ) ;
#5464=LINE ( 'NONE', #19298, #28469 ) ;
#5480=DIRECTION ( 'NONE',  ( -1.174092375852890260E-15, 4.222049128630259891E-16, 1.000000000000000000 ) ) ;
#5526=ADVANCED_FACE ( 'NONE', ( #11841 ), #15595, .T. ) ;
#5529=AXIS2_PLACEMENT_3D ( 'NONE', #13950, #6024, #24940 ) ;
#5532=DIRECTION ( 'NONE',  ( -1.174092375852890260E-15, 4.222049128630259891E-16, 1.000000000000000000 ) ) ;
#5542=ORIENTED_EDGE ( 'NONE', *, *, #16562, .T. ) ;
#5549=VECTOR ( 'NONE', #16666, 1000.000000000000000 ) ;
#5550=AXIS2_PLACEMENT_3D ( 'NONE', #23276, #23653, #18051 ) ;
#5574=PLANE ( 'NONE',  #17617 ) ;
#5633=ORIENTED_EDGE ( 'NONE', *, *, #23519, .T. ) ;
#5667=DIRECTION ( 'NONE',  ( -1.174092375852890260E-15, 4.222049128630259891E-16, 1.000000000000000000 ) ) ;
#5668=( LENGTH_UNIT ( ) NAMED_UNIT ( * ) SI_UNIT ( .MILLI., .METRE. ) );
#5710=DIRECTION ( 'NONE',  ( 1.000000000000000000, -4.524158825347490025E-15, -1.174092375852883357E-15 ) ) ;
#5712=EDGE_CURVE ( 'NONE', #6633, #14626, #35084, .T. ) ;
#5733=LINE ( 'NONE', #13832, #6493 ) ;
#5793=CYLINDRICAL_SURFACE ( 'NONE', #18673, 0.6000000000000028644 ) ;
#5804=CARTESIAN_POINT ( 'NONE',  ( -0.1085714285714300953, -3.798448662927791819, -0.7999999999999951594 ) ) ;
#5852=ORIENTED_EDGE ( 'NONE', *, *, #25069, .T. ) ;
#5866=DIRECTION ( 'NONE',  ( -1.174092375852890260E-15, 4.222049128630259891E-16, 1.000000000000000000 ) ) ;
#5886=VERTEX_POINT ( 'NONE', #33957 ) ;
#5890=CIRCLE ( 'NONE', #4188, 4.872650870659778199 ) ;
#5930=DIRECTION ( 'NONE',  ( 0.02857142857142376188, 0.9995917534020517525, 3.884870526907702485E-16 ) ) ;
#5934=EDGE_CURVE ( 'NONE', #26106, #11426, #34221, .T. ) ;
#6010=CARTESIAN_POINT ( 'NONE',  ( 2.321707774797385326, -4.824281976788927118, -0.7999999999999951594 ) ) ;
#6024=DIRECTION ( 'NONE',  ( 1.174092375852890260E-15, -4.222049128630259891E-16, -1.000000000000000000 ) ) ;
#6057=ORIENTED_EDGE ( 'NONE', *, *, #154, .T. ) ;
#6060=DIRECTION ( 'NONE',  ( 1.000000000000000000, -4.524158825347490025E-15, -1.169797080839617330E-15 ) ) ;
#6082=LINE ( 'NONE', #33445, #8029 ) ;
#6109=AXIS2_PLACEMENT_3D ( 'NONE', #4053, #981, #17703 ) ;
#6118=ORIENTED_EDGE ( 'NONE', *, *, #29358, .T. ) ;
#6182=VECTOR ( 'NONE', #32423, 1000.000000000000000 ) ;
#6319=DIRECTION ( 'NONE',  ( -0.9995917534020514195, -0.02857142857143298367, 1.161550059124387962E-15 ) ) ;
#6365=DIRECTION ( 'NONE',  ( 4.662936703425629071E-15, -1.000000000000000000, 4.222049128630314618E-16 ) ) ;
#6378=EDGE_CURVE ( 'NONE', #20170, #32626, #6535, .T. ) ;
#6427=CARTESIAN_POINT ( 'NONE',  ( 4.747884751462025044, -5.143694235356003119, 0.000000000000000000 ) ) ;
#6451=EDGE_CURVE ( 'NONE', #26552, #17521, #22199, .T. ) ;
#6461=EDGE_LOOP ( 'NONE', ( #31695, #27909, #33772, #3960 ) ) ;
#6493=VECTOR ( 'NONE', #2695, 1000.000000000000000 ) ;
#6535=LINE ( 'NONE', #8879, #898 ) ;
#6539=FACE_OUTER_BOUND ( 'NONE', #6461, .T. ) ;
#6594=PLANE ( 'NONE',  #19626 ) ;
#6606=AXIS2_PLACEMENT_3D ( 'NONE', #33080, #32532, #5710 ) ;
#6633=VERTEX_POINT ( 'NONE', #26896 ) ;
#6817=ORIENTED_EDGE ( 'NONE', *, *, #13105, .T. ) ;
#6849=VERTEX_POINT ( 'NONE', #30293 ) ;
#6888=DIRECTION ( 'NONE',  ( -1.174092375852890260E-15, 4.222049128630259891E-16, 1.000000000000000000 ) ) ;
#6889=ADVANCED_FACE ( 'NONE', ( #16929 ), #735, .T. ) ;
#6975=LINE ( 'NONE', #26248, #3848 ) ;
#7043=ORIENTED_EDGE ( 'NONE', *, *, #8952, .F. ) ;
#7062=DIRECTION ( 'NONE',  ( 1.000000000000000000, -4.524158825347490025E-15, -1.169797080839617330E-15 ) ) ;
#7128=ORIENTED_EDGE ( 'NONE', *, *, #5712, .T. ) ;
#7155=CARTESIAN_POINT ( 'NONE',  ( 2.141980652367342586, -6.189445006155629869, -0.7999999999999951594 ) ) ;
#7312=EDGE_CURVE ( 'NONE', #6849, #21828, #22232, .T. ) ;
#7342=DIRECTION ( 'NONE',  ( -1.174092375852890260E-15, 4.222049128630259891E-16, 1.000000000000000000 ) ) ;
#7408=CARTESIAN_POINT ( 'NONE',  ( -3.160591952521663028, -3.281206521718052382, -0.7999999999999951594 ) ) ;
#7424=PLANE ( 'NONE',  #27331 ) ;
#7457=DIRECTION ( 'NONE',  ( -1.174092375852890260E-15, 4.222049128630259891E-16, 1.000000000000000000 ) ) ;
#7477=FACE_OUTER_BOUND ( 'NONE', #26328, .T. ) ;
#7494=ORIENTED_EDGE ( 'NONE', *, *, #1630, .F. ) ;
#7502=EDGE_CURVE ( 'NONE', #20170, #7837, #24206, .T. ) ;
#7525=ORIENTED_EDGE ( 'NONE', *, *, #34561, .F. ) ;
#7599=AXIS2_PLACEMENT_3D ( 'NONE', #11234, #28153, #777 ) ;
#7674=DIRECTION ( 'NONE',  ( 1.000000000000000000, -4.528031003192420052E-15, -1.179290629824070178E-15 ) ) ;
#7711=DIRECTION ( 'NONE',  ( 1.000000000000000000, -4.524158825347490025E-15, -1.174092375852883357E-15 ) ) ;
#7772=DIRECTION ( 'NONE',  ( 1.000000000000000000, -4.524158825347490025E-15, -1.174092375852883357E-15 ) ) ;
#7788=ORIENTED_EDGE ( 'NONE', *, *, #18922, .F. ) ;
#7837=VERTEX_POINT ( 'NONE', #32175 ) ;
#7904=CARTESIAN_POINT ( 'NONE',  ( -2.321707774797454604, -4.824281976789094095, -0.7999999999999951594 ) ) ;
#7956=CARTESIAN_POINT ( 'NONE',  ( 0.9999999999999453770, -6.008326913195871199, -0.7999999999999951594 ) ) ;
#7958=CIRCLE ( 'NONE', #23484, 2.447112362156711018 ) ;
#7967=EDGE_CURVE ( 'NONE', #3021, #15081, #27308, .T. ) ;
#8016=VERTEX_POINT ( 'NONE', #2312 ) ;
#8029=VECTOR ( 'NONE', #3403, 1000.000000000000000 ) ;
#8113=EDGE_LOOP ( 'NONE', ( #28621, #12995, #16890, #23449 ) ) ;
#8159=CARTESIAN_POINT ( 'NONE',  ( -2.321707774797454604, -4.824281976789094095, -0.7999999999999951594 ) ) ;
#8255=CARTESIAN_POINT ( 'NONE',  ( -1.000000000000014655, -4.808326913196006913, 0.000000000000000000 ) ) ;
#8258=DIRECTION ( 'NONE',  ( -1.174092375852890260E-15, 4.222049128630259891E-16, 1.000000000000000000 ) ) ;
#8259=LINE ( 'NONE', #16882, #26706 ) ;
#8318=CARTESIAN_POINT ( 'NONE',  ( 0.9999999999999453770, -6.008326913195871199, -0.7999999999999951594 ) ) ;
#8332=CARTESIAN_POINT ( 'NONE',  ( -2.321707774797454604, -4.824281976789094095, -0.7999999999999951594 ) ) ;
#8342=SURFACE_SIDE_STYLE ('',( #24753 ) ) ;
#8375=AXIS2_PLACEMENT_3D ( 'NONE', #30144, #5480, #16434 ) ;
#8434=DIRECTION ( 'NONE',  ( 0.02857142857142376188, 0.9995917534020517525, 3.884870526907702485E-16 ) ) ;
#8465=FILL_AREA_STYLE ('',( #24856 ) ) ;
#8484=VECTOR ( 'NONE', #27415, 1000.000000000000000 ) ;
#8566=EDGE_CURVE ( 'NONE', #28118, #17419, #11494, .T. ) ;
#8605=ADVANCED_FACE ( 'NONE', ( #30235 ), #5574, .T. ) ;
#8645=EDGE_CURVE ( 'NONE', #17521, #14609, #21757, .T. ) ;
#8711=DIRECTION ( 'NONE',  ( 1.000000000000000000, -4.625929269271460867E-15, -1.156482317317865217E-15 ) ) ;
#8785=CARTESIAN_POINT ( 'NONE',  ( -2.321707774797454604, -4.824281976789094095, 0.000000000000000000 ) ) ;
#8856=ORIENTED_EDGE ( 'NONE', *, *, #31967, .F. ) ;
#8879=CARTESIAN_POINT ( 'NONE',  ( -2.321707774797454604, -4.824281976789094095, -0.7999999999999951594 ) ) ;
#8880=CYLINDRICAL_SURFACE ( 'NONE', #418, 4.872650870659778199 ) ;
#8921=FACE_OUTER_BOUND ( 'NONE', #8113, .T. ) ;
#8926=CARTESIAN_POINT ( 'NONE',  ( 0.000000000000000000, 0.000000000000000000, -0.7999999999999951594 ) ) ;
#8936=DIRECTION ( 'NONE',  ( -1.174092375852890260E-15, 4.222049128630259891E-16, 1.000000000000000000 ) ) ;
#8944=DIRECTION ( 'NONE',  ( -1.000000000000000000, 4.524158825347490025E-15, 1.174092375852883357E-15 ) ) ;
#8952=EDGE_CURVE ( 'NONE', #32982, #9372, #6975, .T. ) ;
#9058=CARTESIAN_POINT ( 'NONE',  ( -1.566204647097432900, -6.822536405429440620, 0.000000000000000000 ) ) ;
#9105=AXIS2_PLACEMENT_3D ( 'NONE', #2393, #13716, #24695 ) ;
#9150=ORIENTED_EDGE ( 'NONE', *, *, #23606, .F. ) ;
#9196=ORIENTED_EDGE ( 'NONE', *, *, #12339, .T. ) ;
#9200=CARTESIAN_POINT ( 'NONE',  ( 3.799999999999999378, -1.702292157117525034E-14, 4.461551028240974192E-15 ) ) ;
#9206=DIRECTION ( 'NONE',  ( -0.9995917534020514195, -0.02857142857143298367, 1.161550059124387962E-15 ) ) ;
#9322=CARTESIAN_POINT ( 'NONE',  ( -3.160591952521663028, -3.281206521718052382, -0.7999999999999951594 ) ) ;
#9328=CARTESIAN_POINT ( 'NONE',  ( 2.321707774797385326, -4.824281976788927118, 0.000000000000000000 ) ) ;
#9360=CARTESIAN_POINT ( 'NONE',  ( 0.9999999999999731326, -4.808326913196006913, 0.000000000000000000 ) ) ;
#9372=VERTEX_POINT ( 'NONE', #19322 ) ;
#9378=AXIS2_PLACEMENT_3D ( 'NONE', #34124, #7457, #31946 ) ;
#9423=ORIENTED_EDGE ( 'NONE', *, *, #19827, .T. ) ;
#9446=EDGE_CURVE ( 'NONE', #27376, #21688, #35208, .T. ) ;
#9454=DIRECTION ( 'NONE',  ( -1.000000000000000000, 4.625929269271460867E-15, 1.156482317317865217E-15 ) ) ;
#9458=VECTOR ( 'NONE', #1060, 1000.000000000000000 ) ;
#9459=DIRECTION ( 'NONE',  ( 1.000000000000000000, -4.524158825347490025E-15, -1.177133787269970298E-15 ) ) ;
#9570=ORIENTED_EDGE ( 'NONE', *, *, #29758, .F. ) ;
#9600=ORIENTED_EDGE ( 'NONE', *, *, #8566, .T. ) ;
#9716=CARTESIAN_POINT ( 'NONE',  ( -1.000000000000014655, -4.808326913196006913, -0.7999999999999951594 ) ) ;
#9766=CARTESIAN_POINT ( 'NONE',  ( 1.566204647097418912, -6.822536405429468154, -0.7999999999999951594 ) ) ;
#9779=EDGE_CURVE ( 'NONE', #16466, #22478, #4922, .T. ) ;
#9833=VERTEX_POINT ( 'NONE', #16041 ) ;
#9836=DIRECTION ( 'NONE',  ( -1.174092375852890260E-15, 4.222049128630259891E-16, 1.000000000000000000 ) ) ;
#9905=CIRCLE ( 'NONE', #16206, 3.800000000000018918 ) ;
#9932=ORIENTED_EDGE ( 'NONE', *, *, #5712, .F. ) ;
#9935=EDGE_CURVE ( 'NONE', #35493, #30249, #32448, .T. ) ;
#9992=LINE ( 'NONE', #4085, #15223 ) ;
#10025=DIRECTION ( 'NONE',  ( 0.9995917534020517525, -0.02857142857142376188, -1.185676054145132037E-15 ) ) ;
#10077=DIRECTION ( 'NONE',  ( -1.174092375852890260E-15, 4.222049128630259891E-16, 1.000000000000000000 ) ) ;
#10078=DIRECTION ( 'NONE',  ( 1.000000000000000000, -4.625929269271460867E-15, -1.174092375852883357E-15 ) ) ;
#10123=VECTOR ( 'NONE', #22469, 1000.000000000000000 ) ;
#10211=ORIENTED_EDGE ( 'NONE', *, *, #12600, .T. ) ;
#10220=DIRECTION ( 'NONE',  ( 1.000000000000000000, -4.528031003192420052E-15, -1.179290629824070178E-15 ) ) ;
#10225=CIRCLE ( 'NONE', #11379, 0.6000000000000028644 ) ;
#10282=ORIENTED_EDGE ( 'NONE', *, *, #25069, .F. ) ;
#10407=CARTESIAN_POINT ( 'NONE',  ( 1.599999999999989875, -5.408326913195883989, -0.7999999999999958256 ) ) ;
#10410=ORIENTED_EDGE ( 'NONE', *, *, #20014, .F. ) ;
#10426=DIRECTION ( 'NONE',  ( -1.174092375852890260E-15, 4.222049128630259891E-16, 1.000000000000000000 ) ) ;
#10554=APPLICATION_CONTEXT ( 'automotive_design' ) ;
#10639=FACE_OUTER_BOUND ( 'NONE', #14013, .T. ) ;
#10667=DIRECTION ( 'NONE',  ( 1.000000000000000000, -4.524158825347490025E-15, -1.174092375852883357E-15 ) ) ;
#10728=VERTEX_POINT ( 'NONE', #2984 ) ;
#10740=CIRCLE ( 'NONE', #12458, 0.6000000000000029754 ) ;
#10884=ADVANCED_FACE ( 'NONE', ( #16977 ), #17329, .F. ) ;
#10896=ORIENTED_EDGE ( 'NONE', *, *, #7502, .F. ) ;
#10905=DIRECTION ( 'NONE',  ( 1.000000000000000000, -4.336808689941996437E-15, -1.174092375852883357E-15 ) ) ;
#10961=CARTESIAN_POINT ( 'NONE',  ( 0.000000000000000000, 0.000000000000000000, 0.000000000000000000 ) ) ;
#11066=PRESENTATION_STYLE_ASSIGNMENT (( #79 ) ) ;
#11121=DIRECTION ( 'NONE',  ( 1.000000000000000000, -4.524158825347490025E-15, -1.169797080839617330E-15 ) ) ;
#11177=ORIENTED_EDGE ( 'NONE', *, *, #23861, .F. ) ;
#11186=CARTESIAN_POINT ( 'NONE',  ( 0.9999999999999870104, -5.408326913195881325, -0.7999999999999951594 ) ) ;
#11234=CARTESIAN_POINT ( 'NONE',  ( 0.000000000000000000, 0.000000000000000000, -0.7999999999999951594 ) ) ;
#11255=AXIS2_PLACEMENT_3D ( 'NONE', #2535, #8258, #30585 ) ;
#11322=CARTESIAN_POINT ( 'NONE',  ( -0.1085714285714300953, -3.798448662927791819, 0.000000000000000000 ) ) ;
#11379=AXIS2_PLACEMENT_3D ( 'NONE', #1968, #10426, #24455 ) ;
#11426=VERTEX_POINT ( 'NONE', #9200 ) ;
#11450=EDGE_CURVE ( 'NONE', #584, #9372, #3464, .T. ) ;
#11456=LINE ( 'NONE', #32897, #5549 ) ;
#11494=LINE ( 'NONE', #11322, #16465 ) ;
#11519=( NAMED_UNIT ( * ) SI_UNIT ( $, .STERADIAN. ) SOLID_ANGLE_UNIT ( ) );
#11588=DIRECTION ( 'NONE',  ( 0.1305261922200566527, -0.9914448613738098270, -5.718426984394921662E-16 ) ) ;
#11611=LINE ( 'NONE', #22584, #1046 ) ;
#11637=LINE ( 'NONE', #22612, #2040 ) ;
#11717=CIRCLE ( 'NONE', #30164, 4.872650870659778199 ) ;
#11735=ORIENTED_EDGE ( 'NONE', *, *, #12652, .F. ) ;
#11764=DIRECTION ( 'NONE',  ( -1.174092375852890260E-15, 4.222049128630259891E-16, 1.000000000000000000 ) ) ;
#11822=EDGE_LOOP ( 'NONE', ( #4413, #20349, #34788, #4575 ) ) ;
#11841=FACE_OUTER_BOUND ( 'NONE', #20043, .T. ) ;
#11842=ADVANCED_FACE ( 'NONE', ( #673 ), #20452, .F. ) ;
#11949=ORIENTED_EDGE ( 'NONE', *, *, #9935, .T. ) ;
#11952=CARTESIAN_POINT ( 'NONE',  ( -1.387778780781445676E-14, 0.4273491293403097746, -0.7999999999999951594 ) ) ;
#11973=DIRECTION ( 'NONE',  ( 1.174092375852890260E-15, -4.222049128630259891E-16, -1.000000000000000000 ) ) ;
#11995=CARTESIAN_POINT ( 'NONE',  ( 0.000000000000000000, 0.000000000000000000, -0.7999999999999951594 ) ) ;
#12088=CARTESIAN_POINT ( 'NONE',  ( 0.1085714285714300953, -3.798448662927791819, -0.7999999999999951594 ) ) ;
#12093=AXIS2_PLACEMENT_3D ( 'NONE', #34602, #23791, #32596 ) ;
#12118=CARTESIAN_POINT ( 'NONE',  ( 0.000000000000000000, 0.000000000000000000, -0.7999999999999951594 ) ) ;
#12140=ORIENTED_EDGE ( 'NONE', *, *, #20014, .T. ) ;
#12144=EDGE_CURVE ( 'NONE', #28744, #14626, #25415, .T. ) ;
#12192=DIRECTION ( 'NONE',  ( -1.174092375852890457E-15, 4.222049128630259891E-16, 1.000000000000000000 ) ) ;
#12197=( GEOMETRIC_REPRESENTATION_CONTEXT ( 3 ) GLOBAL_UNCERTAINTY_ASSIGNED_CONTEXT ( ( #23214 ) ) GLOBAL_UNIT_ASSIGNED_CONTEXT ( ( #13706, #30608, #14216 ) ) REPRESENTATION_CONTEXT ( 'NONE', 'WORKASPACE' ) );
#12273=ORIENTED_EDGE ( 'NONE', *, *, #27989, .T. ) ;
#12279=CARTESIAN_POINT ( 'NONE',  ( -3.800000000000018918, 1.765716931999654070E-14, -0.7999999999999907185 ) ) ;
#12339=EDGE_CURVE ( 'NONE', #25964, #6849, #9905, .T. ) ;
#12367=CARTESIAN_POINT ( 'NONE',  ( 3.800000000000018918, -1.719180353632054840E-14, -0.7999999999999996003 ) ) ;
#12436=AXIS2_PLACEMENT_3D ( 'NONE', #29662, #21900, #24620 ) ;
#12458=AXIS2_PLACEMENT_3D ( 'NONE', #29990, #32323, #10905 ) ;
#12596=ORIENTED_EDGE ( 'NONE', *, *, #32840, .T. ) ;
#12600=EDGE_CURVE ( 'NONE', #22531, #17419, #28989, .T. ) ;
#12631=EDGE_CURVE ( 'NONE', #15081, #8016, #33345, .T. ) ;
#12639=VECTOR ( 'NONE', #20225, 1000.000000000000000 ) ;
#12641=ORIENTED_EDGE ( 'NONE', *, *, #29358, .F. ) ;
#12652=EDGE_CURVE ( 'NONE', #28118, #27575, #16879, .T. ) ;
#12653=AXIS2_PLACEMENT_3D ( 'NONE', #10961, #21747, #7711 ) ;
#12672=AXIS2_PLACEMENT_3D ( 'NONE', #14630, #6365, #3333 ) ;
#12686=ORIENTED_EDGE ( 'NONE', *, *, #5934, .F. ) ;
#12725=DIRECTION ( 'NONE',  ( 0.000000000000000000, 0.000000000000000000, 1.000000000000000000 ) ) ;
#12942=CARTESIAN_POINT ( 'NONE',  ( -1.387778780781445676E-14, 0.4273491293403097746, -0.7999999999999951594 ) ) ;
#12995=ORIENTED_EDGE ( 'NONE', *, *, #18188, .F. ) ;
#13003=VECTOR ( 'NONE', #28076, 1000.000000000000000 ) ;
#13013=CIRCLE ( 'NONE', #5529, 2.447112362156711018 ) ;
#13035=ORIENTED_EDGE ( 'NONE', *, *, #34064, .F. ) ;
#13037=CIRCLE ( 'NONE', #972, 0.7500000000000039968 ) ;
#13105=EDGE_CURVE ( 'NONE', #21428, #8016, #23908, .T. ) ;
#13157=CARTESIAN_POINT ( 'NONE',  ( 1.398397006337009918, -6.091550361990587525, 0.000000000000000000 ) ) ;
#13223=DIRECTION ( 'NONE',  ( 0.02857142857143298714, -0.9995917534020514195, -4.555780455966493806E-16 ) ) ;
#13244=VECTOR ( 'NONE', #8944, 1000.000000000000000 ) ;
#13254=CARTESIAN_POINT ( 'NONE',  ( -1.000000000000014655, -4.808326913196006913, 0.000000000000000000 ) ) ;
#13329=CARTESIAN_POINT ( 'NONE',  ( 0.000000000000000000, 0.000000000000000000, 0.000000000000000000 ) ) ;
#13345=CIRCLE ( 'NONE', #33444, 7.000000000000035527 ) ;
#13449=EDGE_CURVE ( 'NONE', #3021, #21428, #13037, .T. ) ;
#13489=CARTESIAN_POINT ( 'NONE',  ( -0.1085714285714300953, -3.798448662927791819, 0.000000000000000000 ) ) ;
#13522=EDGE_LOOP ( 'NONE', ( #18379, #27421, #12641, #28216 ) ) ;
#13647=VERTEX_POINT ( 'NONE', #4433 ) ;
#13706=( LENGTH_UNIT ( ) NAMED_UNIT ( * ) SI_UNIT ( .MILLI., .METRE. ) );
#13712=ORIENTED_EDGE ( 'NONE', *, *, #33283, .T. ) ;
#13716=DIRECTION ( 'NONE',  ( -1.174092375852890260E-15, 4.222049128630259891E-16, 1.000000000000000000 ) ) ;
#13762=FACE_OUTER_BOUND ( 'NONE', #20821, .T. ) ;
#13832=CARTESIAN_POINT ( 'NONE',  ( -0.1717365941144438635, -6.008326913195953800, -0.7999999999999951594 ) ) ;
#13907=CIRCLE ( 'NONE', #24834, 3.800000000000018918 ) ;
#13950=CARTESIAN_POINT ( 'NONE',  ( -4.747884751462066788, -5.143694235356003119, -0.7999999999999951594 ) ) ;
#13961=DIRECTION ( 'NONE',  ( -1.174092375852890260E-15, 4.222049128630259891E-16, 1.000000000000000000 ) ) ;
#14013=EDGE_LOOP ( 'NONE', ( #9932, #24406, #6118, #3296 ) ) ;
#14098=ORIENTED_EDGE ( 'NONE', *, *, #22855, .F. ) ;
#14114=CARTESIAN_POINT ( 'NONE',  ( -1.398397006337051440, -6.091550361990532458, -0.7999999999999951594 ) ) ;
#14216=( NAMED_UNIT ( * ) SI_UNIT ( $, .STERADIAN. ) SOLID_ANGLE_UNIT ( ) );
#14250=ORIENTED_EDGE ( 'NONE', *, *, #12339, .F. ) ;
#14307=CARTESIAN_POINT ( 'NONE',  ( 0.1374368770859502042, -4.808326913196061980, 0.000000000000000000 ) ) ;
#14315=CARTESIAN_POINT ( 'NONE',  ( -0.1085714285714300953, -3.798448662927791819, -0.7999999999999951594 ) ) ;
#14329=VERTEX_POINT ( 'NONE', #24064 ) ;
#14415=DIRECTION ( 'NONE',  ( 0.02857142857142376188, 0.9995917534020517525, 3.884870526907702485E-16 ) ) ;
#14504=EDGE_CURVE ( 'NONE', #27575, #3028, #10740, .T. ) ;
#14609=VERTEX_POINT ( 'NONE', #19848 ) ;
#14626=VERTEX_POINT ( 'NONE', #2819 ) ;
#14630=CARTESIAN_POINT ( 'NONE',  ( 0.9999999999999453770, -6.008326913195871199, -0.7999999999999951594 ) ) ;
#14637=AXIS2_PLACEMENT_3D ( 'NONE', #16130, #27149, #2489 ) ;
#14716=EDGE_LOOP ( 'NONE', ( #5633, #7043, #15814, #1204 ) ) ;
#14754=CARTESIAN_POINT ( 'NONE',  ( -0.1085714285714300953, -3.798448662927791819, 0.000000000000000000 ) ) ;
#14760=DIRECTION ( 'NONE',  ( 0.9914448613738109373, -0.1305261922200477154, -1.219156652430115488E-15 ) ) ;
#14779=ADVANCED_FACE ( 'NONE', ( #6539 ), #4397, .F. ) ;
#14961=DIRECTION ( 'NONE',  ( -1.174092375852890260E-15, 4.222049128630259891E-16, 1.000000000000000000 ) ) ;
#14979=CYLINDRICAL_SURFACE ( 'NONE', #1991, 3.800000000000018918 ) ;
#15081=VERTEX_POINT ( 'NONE', #27608 ) ;
#15195=DIRECTION ( 'NONE',  ( 1.174092375852890260E-15, -4.222049128630259891E-16, -1.000000000000000000 ) ) ;
#15220=CARTESIAN_POINT ( 'NONE',  ( 0.2000000000000057288, -6.997142273814354496, -0.7999999999999951594 ) ) ;
#15223=VECTOR ( 'NONE', #1359, 1000.000000000000000 ) ;
#15354=EDGE_LOOP ( 'NONE', ( #35399, #25381, #28991, #16143 ) ) ;
#15407=PLANE ( 'NONE',  #35065 ) ;
#15441=FACE_OUTER_BOUND ( 'NONE', #2010, .T. ) ;
#15453=DIRECTION ( 'NONE',  ( -4.662936703425629071E-15, 1.000000000000000000, -4.222049128630314618E-16 ) ) ;
#15465=VERTEX_POINT ( 'NONE', #7408 ) ;
#15484=CARTESIAN_POINT ( 'NONE',  ( 2.321707774797385326, -4.824281976788927118, -0.7999999999999951594 ) ) ;
#15540=CARTESIAN_POINT ( 'NONE',  ( -2.141980652367370119, -6.189445006155602336, -0.7999999999999951594 ) ) ;
#15558=ORIENTED_EDGE ( 'NONE', *, *, #28400, .F. ) ;
#15595=PLANE ( 'NONE',  #14637 ) ;
#15626=ORIENTED_EDGE ( 'NONE', *, *, #34064, .T. ) ;
#15652=ORIENTED_EDGE ( 'NONE', *, *, #20955, .T. ) ;
#15670=ORIENTED_EDGE ( 'NONE', *, *, #231, .F. ) ;
#15723=DIRECTION ( 'NONE',  ( -1.174092375852890260E-15, 4.222049128630259891E-16, 1.000000000000000000 ) ) ;
#15734=CARTESIAN_POINT ( 'NONE',  ( -3.799999999999999378, 1.782605128514165574E-14, -4.461551028240973403E-15 ) ) ;
#15769=DIRECTION ( 'NONE',  ( 1.000000000000000000, -4.524158825347490025E-15, -1.174092375852883357E-15 ) ) ;
#15781=ORIENTED_EDGE ( 'NONE', *, *, #33075, .F. ) ;
#15788=EDGE_LOOP ( 'NONE', ( #30447, #6057, #16544, #7494 ) ) ;
#15814=ORIENTED_EDGE ( 'NONE', *, *, #28519, .T. ) ;
#15850=VECTOR ( 'NONE', #25271, 1000.000000000000000 ) ;
#15963=DIRECTION ( 'NONE',  ( 1.000000000000000000, -4.524158825347490025E-15, -1.174092375852883357E-15 ) ) ;
#15974=ORIENTED_EDGE ( 'NONE', *, *, #12631, .T. ) ;
#16041=CARTESIAN_POINT ( 'NONE',  ( -4.872650870659766653, 0.4273491293403325897, -0.8000000000000009326 ) ) ;
#16130=CARTESIAN_POINT ( 'NONE',  ( -0.1085714285714300953, -3.798448662927791819, -0.7999999999999951594 ) ) ;
#16143=ORIENTED_EDGE ( 'NONE', *, *, #231, .T. ) ;
#16206=AXIS2_PLACEMENT_3D ( 'NONE', #28759, #4112, #18653 ) ;
#16274=CIRCLE ( 'NONE', #9378, 4.872650870659778199 ) ;
#16383=CLOSED_SHELL ( 'NONE', ( #24545, #29918, #24065, #33900, #24255, #19593, #6889, #14779, #5526, #18108, #24210, #8605, #27571, #29183, #11842, #22226, #34707, #28660, #35101, #32015, #27196, #35365, #19850, #31699, #10884, #24513, #17335 ) ) ;
#16434=DIRECTION ( 'NONE',  ( 1.000000000000000000, -4.336808689941997226E-15, -1.084202172485499306E-15 ) ) ;
#16457=CIRCLE ( 'NONE', #12436, 0.6000000000000029754 ) ;
#16465=VECTOR ( 'NONE', #8434, 999.9999999999998863 ) ;
#16466=VERTEX_POINT ( 'NONE', #19650 ) ;
#16544=ORIENTED_EDGE ( 'NONE', *, *, #23861, .T. ) ;
#16562=EDGE_CURVE ( 'NONE', #18057, #30963, #25662, .T. ) ;
#16666=DIRECTION ( 'NONE',  ( -1.174092375852890260E-15, 4.222049128630259891E-16, 1.000000000000000000 ) ) ;
#16677=EDGE_CURVE ( 'NONE', #35493, #31626, #34478, .T. ) ;
#16704=ORIENTED_EDGE ( 'NONE', *, *, #11450, .T. ) ;
#16706=DIRECTION ( 'NONE',  ( -1.000000000000000000, 4.524158825347490025E-15, 1.174092375852883357E-15 ) ) ;
#16841=CARTESIAN_POINT ( 'NONE',  ( -3.799999999999999378, 1.782605128514165574E-14, -0.7999999999999996003 ) ) ;
#16869=DIRECTION ( 'NONE',  ( -1.174092375852890260E-15, 4.222049128630259891E-16, 1.000000000000000000 ) ) ;
#16879=LINE ( 'NONE', #8255, #4638 ) ;
#16882=CARTESIAN_POINT ( 'NONE',  ( -1.000000000000014655, -4.808326913196006913, 0.000000000000000000 ) ) ;
#16890=ORIENTED_EDGE ( 'NONE', *, *, #22855, .T. ) ;
#16929=FACE_OUTER_BOUND ( 'NONE', #34555, .T. ) ;
#16977=FACE_OUTER_BOUND ( 'NONE', #14716, .T. ) ;
#16978=CARTESIAN_POINT ( 'NONE',  ( 0.000000000000000000, 0.000000000000000000, -0.7999999999999951594 ) ) ;
#16998=DIRECTION ( 'NONE',  ( 1.000000000000000000, -4.524158825347490025E-15, -1.174092375852883357E-15 ) ) ;
#17067=ORIENTED_EDGE ( 'NONE', *, *, #5443, .F. ) ;
#17201=ORIENTED_EDGE ( 'NONE', *, *, #14504, .F. ) ;
#17236=LINE ( 'NONE', #9328, #10123 ) ;
#17329=PLANE ( 'NONE',  #12672 ) ;
#17335=ADVANCED_FACE ( 'NONE', ( #4154 ), #34399, .F. ) ;
#17368=DIRECTION ( 'NONE',  ( -1.174092375852890260E-15, 4.222049128630259891E-16, 1.000000000000000000 ) ) ;
#17393=ORIENTED_EDGE ( 'NONE', *, *, #8952, .T. ) ;
#17419=VERTEX_POINT ( 'NONE', #13489 ) ;
#17485=AXIS2_PLACEMENT_3D ( 'NONE', #24747, #33541, #30674 ) ;
#17497=CARTESIAN_POINT ( 'NONE',  ( -1.000000000000000888, -6.008326913195953800, 0.000000000000000000 ) ) ;
#17521=VERTEX_POINT ( 'NONE', #21397 ) ;
#17544=DIRECTION ( 'NONE',  ( 1.000000000000000000, -4.528031003192420052E-15, -1.179290629824070178E-15 ) ) ;
#17563=EDGE_CURVE ( 'NONE', #10728, #24139, #6082, .T. ) ;
#17570=DIRECTION ( 'NONE',  ( -4.662936703425629071E-15, 1.000000000000000000, -4.222049128630314618E-16 ) ) ;
#17590=LINE ( 'NONE', #25728, #9458 ) ;
#17599=ORIENTED_EDGE ( 'NONE', *, *, #23519, .F. ) ;
#17617=AXIS2_PLACEMENT_3D ( 'NONE', #7904, #19061, #27189 ) ;
#17663=PLANE ( 'NONE',  #34338 ) ;
#17703=DIRECTION ( 'NONE',  ( 1.000000000000000000, -4.625929269271460079E-15, -1.156482317317865020E-15 ) ) ;
#17901=UNCERTAINTY_MEASURE_WITH_UNIT (LENGTH_MEASURE( 1.000000000000000082E-05 ), #5668, 'distance_accuracy_value', 'NONE');
#18011=FACE_OUTER_BOUND ( 'NONE', #2952, .T. ) ;
#18012=VECTOR ( 'NONE', #36, 1000.000000000000000 ) ;
#18051=DIRECTION ( 'NONE',  ( 1.000000000000000000, -4.524158825347490025E-15, -1.169797080839617330E-15 ) ) ;
#18057=VERTEX_POINT ( 'NONE', #14307 ) ;
#18108=ADVANCED_FACE ( 'NONE', ( #33575 ), #19187, .T. ) ;
#18148=ORIENTED_EDGE ( 'NONE', *, *, #33075, .T. ) ;
#18188=EDGE_CURVE ( 'NONE', #31626, #24139, #11611, .T. ) ;
#18199=ORIENTED_EDGE ( 'NONE', *, *, #154, .F. ) ;
#18203=LINE ( 'NONE', #12279, #4643 ) ;
#18292=DIRECTION ( 'NONE',  ( 1.000000000000000000, 0.000000000000000000, 0.000000000000000000 ) ) ;
#18297=ORIENTED_EDGE ( 'NONE', *, *, #13449, .T. ) ;
#18310=CARTESIAN_POINT ( 'NONE',  ( -1.387778780781445676E-14, 0.4273491293403097746, -0.7999999999999951594 ) ) ;
#18320=VERTEX_POINT ( 'NONE', #20226 ) ;
#18379=ORIENTED_EDGE ( 'NONE', *, *, #35124, .T. ) ;
#18401=CARTESIAN_POINT ( 'NONE',  ( 0.9999999999999453770, -6.008326913195871199, -0.7999999999999951594 ) ) ;
#18456=CYLINDRICAL_SURFACE ( 'NONE', #32518, 2.447112362156711018 ) ;
#18519=EDGE_CURVE ( 'NONE', #14609, #13647, #20029, .T. ) ;
#18624=( NAMED_UNIT ( * ) PLANE_ANGLE_UNIT ( ) SI_UNIT ( $, .RADIAN. ) );
#18653=DIRECTION ( 'NONE',  ( 1.000000000000000000, -4.524158825347490025E-15, -1.169797080839617330E-15 ) ) ;
#18673=AXIS2_PLACEMENT_3D ( 'NONE', #11186, #19621, #35516 ) ;
#18674=ORIENTED_EDGE ( 'NONE', *, *, #30183, .F. ) ;
#18678=ORIENTED_EDGE ( 'NONE', *, *, #35264, .F. ) ;
#18685=EDGE_CURVE ( 'NONE', #24050, #18057, #899, .T. ) ;
#18718=VERTEX_POINT ( 'NONE', #9360 ) ;
#18922=EDGE_CURVE ( 'NONE', #22807, #26552, #4511, .T. ) ;
#19031=PLANE ( 'NONE',  #6606 ) ;
#19061=DIRECTION ( 'NONE',  ( -0.9914448613738098270, -0.1305261922200566527, 1.108939053204896328E-15 ) ) ;
#19081=CARTESIAN_POINT ( 'NONE',  ( 0.1717365941144993746, -6.008326913195982222, -0.7999999999999951594 ) ) ;
#19090=AXIS2_PLACEMENT_3D ( 'NONE', #4707, #27013, #10078 ) ;
#19187=CYLINDRICAL_SURFACE ( 'NONE', #21740, 7.000000000000035527 ) ;
#19221=ORIENTED_EDGE ( 'NONE', *, *, #18685, .T. ) ;
#19263=CARTESIAN_POINT ( 'NONE',  ( 0.9999999999999870104, -5.408326913195881325, 0.000000000000000000 ) ) ;
#19291=ORIENTED_EDGE ( 'NONE', *, *, #27810, .F. ) ;
#19298=CARTESIAN_POINT ( 'NONE',  ( 0.1085714285714300953, -3.798448662927791819, -0.7999999999999951594 ) ) ;
#19322=CARTESIAN_POINT ( 'NONE',  ( -0.1717365941144438635, -6.008326913195953800, -0.7999999999999951594 ) ) ;
#19336=DIRECTION ( 'NONE',  ( -1.174092375852890260E-15, 4.222049128630259891E-16, 1.000000000000000000 ) ) ;
#19459=CARTESIAN_POINT ( 'NONE',  ( 0.000000000000000000, 0.000000000000000000, 0.000000000000000000 ) ) ;
#19460=EDGE_CURVE ( 'NONE', #6849, #11426, #1574, .T. ) ;
#19500=VECTOR ( 'NONE', #27837, 1000.000000000000000 ) ;
#19511=DIRECTION ( 'NONE',  ( 1.000000000000000000, -4.607758420995283758E-15, -1.196244974681468005E-15 ) ) ;
#19581=DIRECTION ( 'NONE',  ( 1.000000000000000000, -4.524158825347490025E-15, -1.169797080839617330E-15 ) ) ;
#19593=ADVANCED_FACE ( 'NONE', ( #4469 ), #15407, .T. ) ;
#19621=DIRECTION ( 'NONE',  ( -1.174092375852890260E-15, 4.222049128630259891E-16, 1.000000000000000000 ) ) ;
#19626=AXIS2_PLACEMENT_3D ( 'NONE', #3562, #17570, #12192 ) ;
#19650=CARTESIAN_POINT ( 'NONE',  ( -0.1374368770859779598, -4.808326913195978491, -0.7999999999999951594 ) ) ;
#19719=DIRECTION ( 'NONE',  ( 1.000000000000000000, -4.607758420995283758E-15, -1.174092375852883160E-15 ) ) ;
#19758=LINE ( 'NONE', #1070, #3356 ) ;
#19827=EDGE_CURVE ( 'NONE', #9833, #13647, #30709, .T. ) ;
#19848=CARTESIAN_POINT ( 'NONE',  ( 4.872650870659739120, 0.4273491293402878477, 5.720942237434551585E-15 ) ) ;
#19850=ADVANCED_FACE ( 'NONE', ( #3528 ), #3175, .F. ) ;
#19851=ORIENTED_EDGE ( 'NONE', *, *, #12600, .F. ) ;
#19881=CARTESIAN_POINT ( 'NONE',  ( 1.398397006337009918, -6.091550361990587525, -0.7999999999999951594 ) ) ;
#19894=DIRECTION ( 'NONE',  ( 1.174092375852890260E-15, -4.222049128630259891E-16, -1.000000000000000000 ) ) ;
#19935=VECTOR ( 'NONE', #3645, 1000.000000000000000 ) ;
#20014=EDGE_CURVE ( 'NONE', #32626, #24291, #1526, .T. ) ;
#20024=CARTESIAN_POINT ( 'NONE',  ( -1.387778780781445676E-14, 0.4273491293403097746, -0.7999999999999951594 ) ) ;
#20029=CIRCLE ( 'NONE', #9105, 4.872650870659778199 ) ;
#20030=DIRECTION ( 'NONE',  ( 1.000000000000000000, -4.524158825347490025E-15, -1.177133787269970298E-15 ) ) ;
#20043=EDGE_LOOP ( 'NONE', ( #17599, #31481, #18674, #16704 ) ) ;
#20071=LINE ( 'NONE', #31082, #32493 ) ;
#20170=VERTEX_POINT ( 'NONE', #8159 ) ;
#20206=FACE_OUTER_BOUND ( 'NONE', #34031, .T. ) ;
#20215=MECHANICAL_DESIGN_GEOMETRIC_PRESENTATION_REPRESENTATION('',(#3012),#29452);
#20225=DIRECTION ( 'NONE',  ( -1.174092375852890260E-15, 4.222049128630259891E-16, 1.000000000000000000 ) ) ;
#20226=CARTESIAN_POINT ( 'NONE',  ( 0.9999999999999731326, -4.808326913196006913, -0.7999999999999951594 ) ) ;
#20237=CARTESIAN_POINT ( 'NONE',  ( -1.387778780781445676E-14, 0.4273491293403097746, -0.7999999999999951594 ) ) ;
#20267=VERTEX_POINT ( 'NONE', #26922 ) ;
#20269=DIRECTION ( 'NONE',  ( 1.174092375852890260E-15, -4.222049128630259891E-16, -1.000000000000000000 ) ) ;
#20279=DIRECTION ( 'NONE',  ( -1.174092375852890260E-15, 4.222049128630259891E-16, 1.000000000000000000 ) ) ;
#20349=ORIENTED_EDGE ( 'NONE', *, *, #28519, .F. ) ;
#20439=DIRECTION ( 'NONE',  ( 1.000000000000000000, -4.524158825347490025E-15, -1.174092375852883357E-15 ) ) ;
#20441=ORIENTED_EDGE ( 'NONE', *, *, #3378, .F. ) ;
#20452=CYLINDRICAL_SURFACE ( 'NONE', #24820, 2.447112362156710574 ) ;
#20515=FACE_OUTER_BOUND ( 'NONE', #15354, .T. ) ;
#20516=ORIENTED_EDGE ( 'NONE', *, *, #11450, .F. ) ;
#20540=EDGE_LOOP ( 'NONE', ( #4287, #24675, #3466, #32114 ) ) ;
#20547=ORIENTED_EDGE ( 'NONE', *, *, #18188, .T. ) ;
#20555=VECTOR ( 'NONE', #111, 1000.000000000000000 ) ;
#20563=CARTESIAN_POINT ( 'NONE',  ( -2.141980652367370119, -6.189445006155602336, 0.000000000000000000 ) ) ;
#20569=DIRECTION ( 'NONE',  ( -1.174092375852890260E-15, 4.222049128630259891E-16, 1.000000000000000000 ) ) ;
#20618=ORIENTED_EDGE ( 'NONE', *, *, #3378, .T. ) ;
#20622=VECTOR ( 'NONE', #34701, 1000.000000000000000 ) ;
#20635=DIRECTION ( 'NONE',  ( -1.174092375852890260E-15, 4.222049128630259891E-16, 1.000000000000000000 ) ) ;
#20645=EDGE_LOOP ( 'NONE', ( #22494, #9196, #26267, #12686 ) ) ;
#20771=ORIENTED_EDGE ( 'NONE', *, *, #5178, .T. ) ;
#20781=ORIENTED_EDGE ( 'NONE', *, *, #1630, .T. ) ;
#20821=EDGE_LOOP ( 'NONE', ( #796, #10410, #13712, #25298 ) ) ;
#20846=CARTESIAN_POINT ( 'NONE',  ( -2.141980652367370119, -6.189445006155602336, -0.7999999999999951594 ) ) ;
#20955=EDGE_CURVE ( 'NONE', #17521, #9833, #5890, .T. ) ;
#21019=CIRCLE ( 'NONE', #29680, 7.000000000000035527 ) ;
#21044=DIRECTION ( 'NONE',  ( -1.000000000000000000, 4.625929269271460867E-15, 1.174092375852883357E-15 ) ) ;
#21072=CARTESIAN_POINT ( 'NONE',  ( 0.1374368770859640820, -4.808326913196061980, -0.7999999999999951594 ) ) ;
#21127=CARTESIAN_POINT ( 'NONE',  ( 0.1085714285714300953, -3.798448662927791819, -0.7999999999999951594 ) ) ;
#21159=ORIENTED_EDGE ( 'NONE', *, *, #25362, .T. ) ;
#21292=EDGE_LOOP ( 'NONE', ( #31121, #1245, #30600, #29012 ) ) ;
#21307=AXIS2_PLACEMENT_3D ( 'NONE', #26589, #12725, #18292 ) ;
#21355=EDGE_CURVE ( 'NONE', #5886, #14609, #16274, .T. ) ;
#21356=CYLINDRICAL_SURFACE ( 'NONE', #17485, 0.7500000000000039968 ) ;
#21382=DIRECTION ( 'NONE',  ( -1.174092375852890260E-15, 4.222049128630259891E-16, 1.000000000000000000 ) ) ;
#21397=CARTESIAN_POINT ( 'NONE',  ( 4.872650870659739120, 0.4273491293402878477, -0.7999999999999893863 ) ) ;
#21425=DIRECTION ( 'NONE',  ( 0.1305261922200477154, 0.9914448613738109373, 2.653430841701508438E-16 ) ) ;
#21426=CARTESIAN_POINT ( 'NONE',  ( 0.9999999999999453770, -6.008326913195871199, -0.7999999999999951594 ) ) ;
#21428=VERTEX_POINT ( 'NONE', #24212 ) ;
#21506=ORIENTED_EDGE ( 'NONE', *, *, #22416, .T. ) ;
#21542=DIRECTION ( 'NONE',  ( -1.174092375852890260E-15, 4.222049128630259891E-16, 1.000000000000000000 ) ) ;
#21561=EDGE_CURVE ( 'NONE', #30249, #6633, #34733, .T. ) ;
#21595=CYLINDRICAL_SURFACE ( 'NONE', #12093, 0.6000000000000028644 ) ;
#21606=AXIS2_PLACEMENT_3D ( 'NONE', #20024, #20569, #34091 ) ;
#21623=CARTESIAN_POINT ( 'NONE',  ( -1.000000000000014655, -4.808326913196006913, -0.7999999999999951594 ) ) ;
#21635=EDGE_CURVE ( 'NONE', #22478, #27575, #420, .T. ) ;
#21688=VERTEX_POINT ( 'NONE', #9058 ) ;
#21713=DIRECTION ( 'NONE',  ( -1.174092375852890260E-15, 4.222049128630259891E-16, 1.000000000000000000 ) ) ;
#21737=ORIENTED_EDGE ( 'NONE', *, *, #17563, .F. ) ;
#21740=AXIS2_PLACEMENT_3D ( 'NONE', #110, #30710, #281 ) ;
#21747=DIRECTION ( 'NONE',  ( -1.174092375852890260E-15, 4.222049128630259891E-16, 1.000000000000000000 ) ) ;
#21757=LINE ( 'NONE', #27714, #25122 ) ;
#21828=VERTEX_POINT ( 'NONE', #4210 ) ;
#21900=DIRECTION ( 'NONE',  ( -1.174092375852890260E-15, 4.222049128630259891E-16, 1.000000000000000000 ) ) ;
#21943=DIRECTION ( 'NONE',  ( -1.000000000000000000, 4.524158825347490025E-15, 1.174092375852883357E-15 ) ) ;
#21953=AXIS2_PLACEMENT_3D ( 'NONE', #19263, #2750, #24690 ) ;
#22199=CIRCLE ( 'NONE', #21606, 4.872650870659778199 ) ;
#22226=ADVANCED_FACE ( 'NONE', ( #20515 ), #31333, .T. ) ;
#22232=CIRCLE ( 'NONE', #2144, 3.800000000000018918 ) ;
#22376=EDGE_CURVE ( 'NONE', #11426, #24050, #13907, .T. ) ;
#22416=EDGE_CURVE ( 'NONE', #24291, #21688, #4734, .T. ) ;
#22427=CARTESIAN_POINT ( 'NONE',  ( -1.566204647097432900, -6.822536405429440620, -0.7999999999999951594 ) ) ;
#22469=DIRECTION ( 'NONE',  ( 0.1305261922200477154, 0.9914448613738109373, 2.653430841701508438E-16 ) ) ;
#22478=VERTEX_POINT ( 'NONE', #22774 ) ;
#22480=DIRECTION ( 'NONE',  ( -1.174092375852890260E-15, 4.222049128630259891E-16, 1.000000000000000000 ) ) ;
#22494=ORIENTED_EDGE ( 'NONE', *, *, #30609, .F. ) ;
#22531=VERTEX_POINT ( 'NONE', #14315 ) ;
#22584=CARTESIAN_POINT ( 'NONE',  ( 0.2000000000000057288, -6.997142273814354496, -0.7999999999999951594 ) ) ;
#22612=CARTESIAN_POINT ( 'NONE',  ( -0.2000000000000612399, -6.997142273814382030, -0.7999999999999951594 ) ) ;
#22718=MANIFOLD_SOLID_BREP ( 'Notch', #16383 ) ;
#22761=CARTESIAN_POINT ( 'NONE',  ( -4.872650870659791522, 0.4273491293403324232, -0.7999999999999893863 ) ) ;
#22774=CARTESIAN_POINT ( 'NONE',  ( -1.000000000000014655, -4.808326913196006913, -0.7999999999999951594 ) ) ;
#22807=VERTEX_POINT ( 'NONE', #6010 ) ;
#22855=EDGE_CURVE ( 'NONE', #31626, #3021, #3027, .T. ) ;
#23003=EDGE_LOOP ( 'NONE', ( #9150, #15670, #32939, #26728 ) ) ;
#23061=CARTESIAN_POINT ( 'NONE',  ( 0.1717365941144993746, -6.008326913195982222, -0.7999999999999951594 ) ) ;
#23091=ORIENTED_EDGE ( 'NONE', *, *, #22376, .T. ) ;
#23187=EDGE_CURVE ( 'NONE', #10728, #28744, #2235, .T. ) ;
#23214=UNCERTAINTY_MEASURE_WITH_UNIT (LENGTH_MEASURE( 1.000000000000000082E-05 ), #13706, 'distance_accuracy_value', 'NONE');
#23276=CARTESIAN_POINT ( 'NONE',  ( 0.000000000000000000, 0.000000000000000000, -0.7999999999999951594 ) ) ;
#23449=ORIENTED_EDGE ( 'NONE', *, *, #7967, .T. ) ;
#23484=AXIS2_PLACEMENT_3D ( 'NONE', #28382, #19894, #19719 ) ;
#23519=EDGE_CURVE ( 'NONE', #34652, #9372, #5733, .T. ) ;
#23551=EDGE_LOOP ( 'NONE', ( #28330, #23702, #318, #27537, #5342, #12596, #15974, #21159, #2763, #28141, #24902, #20781, #15626, #12273, #21506, #29646, #30010, #15558, #17201, #11735, #9600, #20618, #29820, #23091, #19221 ) ) ;
#23606=EDGE_CURVE ( 'NONE', #14329, #5886, #1940, .T. ) ;
#23653=DIRECTION ( 'NONE',  ( -1.174092375852890260E-15, 4.222049128630259891E-16, 1.000000000000000000 ) ) ;
#23702=ORIENTED_EDGE ( 'NONE', *, *, #25118, .F. ) ;
#23722=( GEOMETRIC_REPRESENTATION_CONTEXT ( 3 ) GLOBAL_UNCERTAINTY_ASSIGNED_CONTEXT ( ( #17901 ) ) GLOBAL_UNIT_ASSIGNED_CONTEXT ( ( #5668, #18624, #29622 ) ) REPRESENTATION_CONTEXT ( 'NONE', 'WORKASPACE' ) );
#23791=DIRECTION ( 'NONE',  ( -1.174092375852890260E-15, 4.222049128630259891E-16, 1.000000000000000000 ) ) ;
#23811=PRODUCT_DEFINITION ( 'UNKNOWN', '', #2336, #24450 ) ;
#23861=EDGE_CURVE ( 'NONE', #15465, #34789, #33996, .T. ) ;
#23893=ORIENTED_EDGE ( 'NONE', *, *, #25118, .T. ) ;
#23908=LINE ( 'NONE', #7155, #1765 ) ;
#24003=FACE_OUTER_BOUND ( 'NONE', #13522, .T. ) ;
#24017=AXIS2_PLACEMENT_3D ( 'NONE', #14114, #25650, #8711 ) ;
#24050=VERTEX_POINT ( 'NONE', #1401 ) ;
#24064=CARTESIAN_POINT ( 'NONE',  ( 2.321707774797385326, -4.824281976788927118, 0.000000000000000000 ) ) ;
#24065=ADVANCED_FACE ( 'NONE', ( #1584 ), #26071, .T. ) ;
#24139=VERTEX_POINT ( 'NONE', #25090 ) ;
#24206=LINE ( 'NONE', #8332, #32035 ) ;
#24210=ADVANCED_FACE ( 'NONE', ( #13762 ), #21356, .T. ) ;
#24212=CARTESIAN_POINT ( 'NONE',  ( 2.141980652367342586, -6.189445006155629869, -0.7999999999999951594 ) ) ;
#24255=ADVANCED_FACE ( 'NONE', ( #1311 ), #14979, .F. ) ;
#24288=VECTOR ( 'NONE', #13961, 1000.000000000000000 ) ;
#24291=VERTEX_POINT ( 'NONE', #20563 ) ;
#24303=DIRECTION ( 'NONE',  ( 1.174092375852890260E-15, -4.222049128630259891E-16, -1.000000000000000000 ) ) ;
#24354=CARTESIAN_POINT ( 'NONE',  ( 0.9999999999999453770, -6.008326913195871199, 0.000000000000000000 ) ) ;
#24406=ORIENTED_EDGE ( 'NONE', *, *, #21561, .F. ) ;
#24450=PRODUCT_DEFINITION_CONTEXT ( 'detailed design', #10554, 'design' ) ;
#24455=DIRECTION ( 'NONE',  ( 1.000000000000000000, -4.336808689941997226E-15, -1.084202172485499306E-15 ) ) ;
#24513=ADVANCED_FACE ( 'NONE', ( #24003 ), #7424, .F. ) ;
#24545=ADVANCED_FACE ( 'NONE', ( #1862 ), #5793, .F. ) ;
#24586=CARTESIAN_POINT ( 'NONE',  ( -4.747884751462066788, -5.143694235356003119, -0.7999999999999951594 ) ) ;
#24620=DIRECTION ( 'NONE',  ( 1.000000000000000000, -4.336808689941996437E-15, -1.084202172485499109E-15 ) ) ;
#24675=ORIENTED_EDGE ( 'NONE', *, *, #8645, .T. ) ;
#24683=SURFACE_STYLE_USAGE ( .BOTH. , #25218 ) ;
#24690=DIRECTION ( 'NONE',  ( 1.000000000000000000, -4.336808689941997226E-15, -1.174092375852883357E-15 ) ) ;
#24695=DIRECTION ( 'NONE',  ( 1.000000000000000000, -4.528031003192420052E-15, -1.174092375852883160E-15 ) ) ;
#24710=CARTESIAN_POINT ( 'NONE',  ( -0.1374368770859779598, -4.808326913195978491, -0.7999999999999951594 ) ) ;
#24729=CIRCLE ( 'NONE', #12653, 7.000000000000035527 ) ;
#24747=CARTESIAN_POINT ( 'NONE',  ( -1.398397006337051440, -6.091550361990532458, -0.7999999999999951594 ) ) ;
#24753=SURFACE_STYLE_FILL_AREA ( #27463 ) ;
#24820=AXIS2_PLACEMENT_3D ( 'NONE', #28588, #16869, #3221 ) ;
#24834=AXIS2_PLACEMENT_3D ( 'NONE', #13329, #4872, #2190 ) ;
#24856=FILL_AREA_STYLE_COLOUR ( '', #32320 ) ;
#24867=CIRCLE ( 'NONE', #29478, 3.800000000000018918 ) ;
#24902=ORIENTED_EDGE ( 'NONE', *, *, #18519, .T. ) ;
#24940=DIRECTION ( 'NONE',  ( 1.000000000000000000, -4.607758420995283758E-15, -1.196244974681468005E-15 ) ) ;
#24983=ORIENTED_EDGE ( 'NONE', *, *, #9779, .F. ) ;
#25032=( NAMED_UNIT ( * ) PLANE_ANGLE_UNIT ( ) SI_UNIT ( $, .RADIAN. ) );
#25069=EDGE_CURVE ( 'NONE', #22531, #25964, #25630, .T. ) ;
#25090=CARTESIAN_POINT ( 'NONE',  ( 0.2000000000000057288, -6.997142273814354496, 0.000000000000000000 ) ) ;
#25118=EDGE_CURVE ( 'NONE', #14626, #18718, #26790, .T. ) ;
#25122=VECTOR ( 'NONE', #27361, 1000.000000000000000 ) ;
#25218=SURFACE_SIDE_STYLE ('',( #28093 ) ) ;
#25271=DIRECTION ( 'NONE',  ( -1.174092375852890260E-15, 4.222049128630259891E-16, 1.000000000000000000 ) ) ;
#25298=ORIENTED_EDGE ( 'NONE', *, *, #9446, .T. ) ;
#25301=AXIS2_PLACEMENT_3D ( 'NONE', #33763, #27667, #28011 ) ;
#25315=PRODUCT_DEFINITION_SHAPE ( 'NONE', 'NONE',  #23811 ) ;
#25362=EDGE_CURVE ( 'NONE', #8016, #14329, #17236, .T. ) ;
#25381=ORIENTED_EDGE ( 'NONE', *, *, #13105, .F. ) ;
#25415=CIRCLE ( 'NONE', #21953, 0.6000000000000028644 ) ;
#25501=DIRECTION ( 'NONE',  ( 1.000000000000000000, -4.524158825347490025E-15, -1.174092375852883357E-15 ) ) ;
#25565=ORIENTED_EDGE ( 'NONE', *, *, #30394, .T. ) ;
#25581=CARTESIAN_POINT ( 'NONE',  ( 0.1085714285714300953, -3.798448662927791819, 0.000000000000000000 ) ) ;
#25596=EDGE_CURVE ( 'NONE', #22478, #32982, #16457, .T. ) ;
#25608=DIRECTION ( 'NONE',  ( 0.02857142857143298367, -0.9995917534020514195, -4.555780455966494792E-16 ) ) ;
#25630=CIRCLE ( 'NONE', #34835, 3.800000000000018918 ) ;
#25650=DIRECTION ( 'NONE',  ( -1.174092375852890260E-15, 4.222049128630259891E-16, 1.000000000000000000 ) ) ;
#25662=LINE ( 'NONE', #993, #26390 ) ;
#25696=ORIENTED_EDGE ( 'NONE', *, *, #938, .F. ) ;
#25728=CARTESIAN_POINT ( 'NONE',  ( 0.9999999999999731326, -4.808326913196006913, -0.7999999999999951594 ) ) ;
#25763=DIRECTION ( 'NONE',  ( 0.02857142857142376188, 0.9995917534020517525, 3.884870526907702485E-16 ) ) ;
#25777=AXIS2_PLACEMENT_3D ( 'NONE', #34942, #24303, #27006 ) ;
#25875=ORIENTED_EDGE ( 'NONE', *, *, #16677, .F. ) ;
#25914=EDGE_LOOP ( 'NONE', ( #839, #10896, #30651, #12140 ) ) ;
#25964=VERTEX_POINT ( 'NONE', #16841 ) ;
#26071=CYLINDRICAL_SURFACE ( 'NONE', #28968, 4.872650870659778199 ) ;
#26089=CYLINDRICAL_SURFACE ( 'NONE', #33820, 3.800000000000018918 ) ;
#26106=VERTEX_POINT ( 'NONE', #15734 ) ;
#26123=ORIENTED_EDGE ( 'NONE', *, *, #18519, .F. ) ;
#26173=CARTESIAN_POINT ( 'NONE',  ( -0.1717365941144438635, -6.008326913195953800, 0.000000000000000000 ) ) ;
#26177=ORIENTED_EDGE ( 'NONE', *, *, #16677, .T. ) ;
#26248=CARTESIAN_POINT ( 'NONE',  ( 0.9999999999999453770, -6.008326913195871199, -0.7999999999999951594 ) ) ;
#26267=ORIENTED_EDGE ( 'NONE', *, *, #19460, .T. ) ;
#26328=EDGE_LOOP ( 'NONE', ( #13035, #11177, #879, #4597 ) ) ;
#26371=DIRECTION ( 'NONE',  ( 0.02857142857143298714, -0.9995917534020514195, -4.555780455966493806E-16 ) ) ;
#26390=VECTOR ( 'NONE', #11973, 1000.000000000000000 ) ;
#26419=CARTESIAN_POINT ( 'NONE',  ( -0.1085714285714300953, -3.798448662927791819, -0.7999999999999951594 ) ) ;
#26470=VECTOR ( 'NONE', #29361, 1000.000000000000000 ) ;
#26552=VERTEX_POINT ( 'NONE', #29719 ) ;
#26589=CARTESIAN_POINT ( 'NONE',  ( 0.000000000000000000, 0.000000000000000000, 0.000000000000000000 ) ) ;
#26630=VECTOR ( 'NONE', #25763, 999.9999999999998863 ) ;
#26706=VECTOR ( 'NONE', #21943, 1000.000000000000000 ) ;
#26728=ORIENTED_EDGE ( 'NONE', *, *, #27311, .T. ) ;
#26790=CIRCLE ( 'NONE', #11255, 0.6000000000000028644 ) ;
#26896=CARTESIAN_POINT ( 'NONE',  ( 1.599999999999986766, -5.408326913195883989, -0.7999999999999944933 ) ) ;
#26922=CARTESIAN_POINT ( 'NONE',  ( -0.2000000000000612399, -6.997142273814382030, 0.000000000000000000 ) ) ;
#27006=DIRECTION ( 'NONE',  ( 1.000000000000000000, -4.607758420995284547E-15, -1.196244974681468202E-15 ) ) ;
#27013=DIRECTION ( 'NONE',  ( -1.174092375852890260E-15, 4.222049128630259891E-16, 1.000000000000000000 ) ) ;
#27035=ORIENTED_EDGE ( 'NONE', *, *, #30609, .T. ) ;
#27125=VECTOR ( 'NONE', #14415, 999.9999999999998863 ) ;
#27149=DIRECTION ( 'NONE',  ( 0.9995917534020517525, -0.02857142857142376188, -1.185676054145132037E-15 ) ) ;
#27167=DIRECTION ( 'NONE',  ( 1.000000000000000000, -4.528031003192420052E-15, -1.179290629824070178E-15 ) ) ;
#27173=ORIENTED_EDGE ( 'NONE', *, *, #6378, .F. ) ;
#27189=DIRECTION ( 'NONE',  ( 0.1305261922200566249, -0.9914448613738097160, -5.718426984394921662E-16 ) ) ;
#27196=ADVANCED_FACE ( 'NONE', ( #125 ), #19031, .T. ) ;
#27308=LINE ( 'NONE', #2478, #20555 ) ;
#27311=EDGE_CURVE ( 'NONE', #26552, #5886, #20071, .T. ) ;
#27331=AXIS2_PLACEMENT_3D ( 'NONE', #18401, #29581, #32272 ) ;
#27361=DIRECTION ( 'NONE',  ( -1.174092375852890260E-15, 4.222049128630259891E-16, 1.000000000000000000 ) ) ;
#27376=VERTEX_POINT ( 'NONE', #22427 ) ;
#27415=DIRECTION ( 'NONE',  ( -1.000000000000000000, 4.524158825347490025E-15, 1.174092375852883357E-15 ) ) ;
#27417=LINE ( 'NONE', #24710, #18012 ) ;
#27421=ORIENTED_EDGE ( 'NONE', *, *, #23187, .T. ) ;
#27463=FILL_AREA_STYLE ('',( #2619 ) ) ;
#27483=ORIENTED_EDGE ( 'NONE', *, *, #33677, .T. ) ;
#27536=LINE ( 'NONE', #2873, #13244 ) ;
#27537=ORIENTED_EDGE ( 'NONE', *, *, #23187, .F. ) ;
#27571=ADVANCED_FACE ( 'NONE', ( #7477 ), #18456, .F. ) ;
#27575=VERTEX_POINT ( 'NONE', #13254 ) ;
#27608=CARTESIAN_POINT ( 'NONE',  ( 1.566204647097418912, -6.822536405429468154, 0.000000000000000000 ) ) ;
#27664=LINE ( 'NONE', #105, #24288 ) ;
#27667=DIRECTION ( 'NONE',  ( -1.174092375852890260E-15, 4.222049128630259891E-16, 1.000000000000000000 ) ) ;
#27714=CARTESIAN_POINT ( 'NONE',  ( 4.872650870659763989, 0.4273491293402877367, -0.8000000000000009326 ) ) ;
#27739=ORIENTED_EDGE ( 'NONE', *, *, #25596, .T. ) ;
#27752=DIRECTION ( 'NONE',  ( 0.02857142857143298714, -0.9995917534020514195, -4.555780455966493806E-16 ) ) ;
#27810=EDGE_CURVE ( 'NONE', #27376, #584, #21019, .T. ) ;
#27837=DIRECTION ( 'NONE',  ( -1.174092375852890260E-15, 4.222049128630259891E-16, 1.000000000000000000 ) ) ;
#27863=PRODUCT_CONTEXT ( 'NONE', #3200, 'mechanical' ) ;
#27896=CIRCLE ( 'NONE', #3739, 4.872650870659778199 ) ;
#27909=ORIENTED_EDGE ( 'NONE', *, *, #7312, .T. ) ;
#27919=DIRECTION ( 'NONE',  ( 1.000000000000000000, -4.524158825347490025E-15, -1.174092375852883357E-15 ) ) ;
#27934=DIRECTION ( 'NONE',  ( 0.02857142857143298367, -0.9995917534020514195, -4.555780455966494792E-16 ) ) ;
#27972=AXIS2_PLACEMENT_3D ( 'NONE', #31529, #6319, #27934 ) ;
#27989=EDGE_CURVE ( 'NONE', #7837, #24291, #32941, .T. ) ;
#28011=DIRECTION ( 'NONE',  ( 1.000000000000000000, -4.336808689941996437E-15, -1.084202172485499109E-15 ) ) ;
#28027=DIRECTION ( 'NONE',  ( -1.174092375852890260E-15, 4.222049128630259891E-16, 1.000000000000000000 ) ) ;
#28076=DIRECTION ( 'NONE',  ( 0.1305261922200566527, -0.9914448613738098270, -5.718426984394921662E-16 ) ) ;
#28093=SURFACE_STYLE_FILL_AREA ( #8465 ) ;
#28118=VERTEX_POINT ( 'NONE', #5409 ) ;
#28141=ORIENTED_EDGE ( 'NONE', *, *, #21355, .T. ) ;
#28153=DIRECTION ( 'NONE',  ( -1.174092375852890260E-15, 4.222049128630259891E-16, 1.000000000000000000 ) ) ;
#28216=ORIENTED_EDGE ( 'NONE', *, *, #9935, .F. ) ;
#28291=AXIS2_PLACEMENT_3D ( 'NONE', #35593, #30009, #16998 ) ;
#28330=ORIENTED_EDGE ( 'NONE', *, *, #5178, .F. ) ;
#28382=CARTESIAN_POINT ( 'NONE',  ( -4.747884751462066788, -5.143694235356003119, 0.000000000000000000 ) ) ;
#28396=VECTOR ( 'NONE', #20279, 1000.000000000000000 ) ;
#28400=EDGE_CURVE ( 'NONE', #3028, #34652, #5008, .T. ) ;
#28469=VECTOR ( 'NONE', #13223, 1000.000000000000000 ) ;
#28519=EDGE_CURVE ( 'NONE', #32982, #3028, #11456, .T. ) ;
#28546=EDGE_LOOP ( 'NONE', ( #32983, #30357, #28564, #24983 ) ) ;
#28564=ORIENTED_EDGE ( 'NONE', *, *, #21635, .F. ) ;
#28586=VECTOR ( 'NONE', #5667, 1000.000000000000000 ) ;
#28588=CARTESIAN_POINT ( 'NONE',  ( 4.747884751462025044, -5.143694235356003119, -0.7999999999999951594 ) ) ;
#28621=ORIENTED_EDGE ( 'NONE', *, *, #32840, .F. ) ;
#28631=UNCERTAINTY_MEASURE_WITH_UNIT (LENGTH_MEASURE( 1.000000000000000082E-05 ), #30444, 'distance_accuracy_value', 'NONE');
#28660=ADVANCED_FACE ( 'NONE', ( #8921 ), #4089, .T. ) ;
#28744=VERTEX_POINT ( 'NONE', #33782 ) ;
#28757=EDGE_LOOP ( 'NONE', ( #3975, #5252, #18148, #35331, #29744, #14250, #10282, #31220, #29888, #27739, #17393, #20516, #19291, #5236, #27173, #7525, #18199, #31825, #30339, #7788, #18678, #32556, #14098, #25875, #11949 ) ) ;
#28759=CARTESIAN_POINT ( 'NONE',  ( 0.000000000000000000, 0.000000000000000000, -0.7999999999999951594 ) ) ;
#28785=ORIENTED_EDGE ( 'NONE', *, *, #35124, .F. ) ;
#28968=AXIS2_PLACEMENT_3D ( 'NONE', #18310, #20635, #10220 ) ;
#28989=LINE ( 'NONE', #1989, #26470 ) ;
#28991=ORIENTED_EDGE ( 'NONE', *, *, #35264, .T. ) ;
#29012=ORIENTED_EDGE ( 'NONE', *, *, #30183, .T. ) ;
#29075=PRODUCT ( 'circlip for shafts normal_din_Circlip DIN 471 - 8 x 0.8', 'circlip for shafts normal_din_Circlip DIN 471 - 8 x 0.8', '', ( #27863 ) ) ;
#29183=ADVANCED_FACE ( 'NONE', ( #33379 ), #8880, .T. ) ;
#29358=EDGE_CURVE ( 'NONE', #30249, #28744, #29907, .T. ) ;
#29361=DIRECTION ( 'NONE',  ( -1.174092375852890260E-15, 4.222049128630259891E-16, 1.000000000000000000 ) ) ;
#29452=( GEOMETRIC_REPRESENTATION_CONTEXT ( 3 ) GLOBAL_UNCERTAINTY_ASSIGNED_CONTEXT ( ( #28631 ) ) GLOBAL_UNIT_ASSIGNED_CONTEXT ( ( #30444, #25032, #11519 ) ) REPRESENTATION_CONTEXT ( 'NONE', 'WORKASPACE' ) );
#29478=AXIS2_PLACEMENT_3D ( 'NONE', #19459, #3447, #27919 ) ;
#29496=EDGE_LOOP ( 'NONE', ( #5542, #15781, #5291, #20771 ) ) ;
#29581=DIRECTION ( 'NONE',  ( 4.662936703425629071E-15, -1.000000000000000000, 4.222049128630314618E-16 ) ) ;
#29622=( NAMED_UNIT ( * ) SI_UNIT ( $, .STERADIAN. ) SOLID_ANGLE_UNIT ( ) );
#29646=ORIENTED_EDGE ( 'NONE', *, *, #31673, .T. ) ;
#29662=CARTESIAN_POINT ( 'NONE',  ( -1.000000000000014655, -5.408326913195881325, -0.7999999999999951594 ) ) ;
#29680=AXIS2_PLACEMENT_3D ( 'NONE', #16978, #11764, #20030 ) ;
#29719=CARTESIAN_POINT ( 'NONE',  ( 3.160591952521676795, -3.281206521718066149, -0.7999999999999951594 ) ) ;
#29744=ORIENTED_EDGE ( 'NONE', *, *, #7312, .F. ) ;
#29758=EDGE_CURVE ( 'NONE', #6633, #18320, #10225, .T. ) ;
#29820=ORIENTED_EDGE ( 'NONE', *, *, #5934, .T. ) ;
#29888=ORIENTED_EDGE ( 'NONE', *, *, #9779, .T. ) ;
#29901=EDGE_LOOP ( 'NONE', ( #5852, #27035, #20441, #19851 ) ) ;
#29907=LINE ( 'NONE', #21426, #6182 ) ;
#29918=ADVANCED_FACE ( 'NONE', ( #15441 ), #35103, .T. ) ;
#29952=ORIENTED_EDGE ( 'NONE', *, *, #7967, .F. ) ;
#29990=CARTESIAN_POINT ( 'NONE',  ( -1.000000000000014655, -5.408326913195881325, 0.000000000000000000 ) ) ;
#30004=ORIENTED_EDGE ( 'NONE', *, *, #8645, .F. ) ;
#30009=DIRECTION ( 'NONE',  ( 1.174092375852885330E-15, 4.222049128630153888E-16, 1.000000000000000000 ) ) ;
#30010=ORIENTED_EDGE ( 'NONE', *, *, #3606, .T. ) ;
#30144=CARTESIAN_POINT ( 'NONE',  ( 0.9999999999999870104, -5.408326913195881325, -0.7999999999999951594 ) ) ;
#30164=AXIS2_PLACEMENT_3D ( 'NONE', #33833, #22480, #30253 ) ;
#30178=PLANE ( 'NONE',  #28291 ) ;
#30183=EDGE_CURVE ( 'NONE', #584, #20267, #11637, .T. ) ;
#30235=FACE_OUTER_BOUND ( 'NONE', #25914, .T. ) ;
#30249=VERTEX_POINT ( 'NONE', #8318 ) ;
#30253=DIRECTION ( 'NONE',  ( 1.000000000000000000, -4.528031003192420052E-15, -1.174092375852883160E-15 ) ) ;
#30293=CARTESIAN_POINT ( 'NONE',  ( 3.799999999999999378, -1.702292157117525034E-14, -0.7999999999999907185 ) ) ;
#30335=CARTESIAN_POINT ( 'NONE',  ( -1.566204647097432900, -6.822536405429440620, -0.7999999999999951594 ) ) ;
#30339=ORIENTED_EDGE ( 'NONE', *, *, #6451, .F. ) ;
#30357=ORIENTED_EDGE ( 'NONE', *, *, #12652, .T. ) ;
#30394=EDGE_CURVE ( 'NONE', #21828, #30963, #5464, .T. ) ;
#30408=CARTESIAN_POINT ( 'NONE',  ( -1.000000000000000888, -6.008326913195953800, -0.7999999999999951594 ) ) ;
#30444=( LENGTH_UNIT ( ) NAMED_UNIT ( * ) SI_UNIT ( .MILLI., .METRE. ) );
#30447=ORIENTED_EDGE ( 'NONE', *, *, #19827, .F. ) ;
#30568=DIRECTION ( 'NONE',  ( 1.000000000000000000, -4.607758420995284547E-15, -1.174092375852883357E-15 ) ) ;
#30585=DIRECTION ( 'NONE',  ( 1.000000000000000000, -4.336808689941997226E-15, -1.174092375852883357E-15 ) ) ;
#30600=ORIENTED_EDGE ( 'NONE', *, *, #27810, .T. ) ;
#30608=( NAMED_UNIT ( * ) PLANE_ANGLE_UNIT ( ) SI_UNIT ( $, .RADIAN. ) );
#30609=EDGE_CURVE ( 'NONE', #25964, #26106, #18203, .T. ) ;
#30651=ORIENTED_EDGE ( 'NONE', *, *, #6378, .T. ) ;
#30674=DIRECTION ( 'NONE',  ( 1.000000000000000000, -4.625929269271460867E-15, -1.156482317317865217E-15 ) ) ;
#30709=LINE ( 'NONE', #22761, #19500 ) ;
#30710=DIRECTION ( 'NONE',  ( -1.174092375852890260E-15, 4.222049128630259891E-16, 1.000000000000000000 ) ) ;
#30963=VERTEX_POINT ( 'NONE', #21072 ) ;
#30981=ORIENTED_EDGE ( 'NONE', *, *, #8566, .F. ) ;
#31057=AXIS2_PLACEMENT_3D ( 'NONE', #13157, #10077, #21044 ) ;
#31082=CARTESIAN_POINT ( 'NONE',  ( 3.160591952521676795, -3.281206521718066149, -0.7999999999999951594 ) ) ;
#31121=ORIENTED_EDGE ( 'NONE', *, *, #31673, .F. ) ;
#31220=ORIENTED_EDGE ( 'NONE', *, *, #33677, .F. ) ;
#31247=DIRECTION ( 'NONE',  ( -1.174092375852890260E-15, 4.222049128630259891E-16, 1.000000000000000000 ) ) ;
#31272=CARTESIAN_POINT ( 'NONE',  ( 0.000000000000000000, 0.000000000000000000, 0.000000000000000000 ) ) ;
#31328=LINE ( 'NONE', #14754, #26630 ) ;
#31333=PLANE ( 'NONE',  #32545 ) ;
#31455=FACE_OUTER_BOUND ( 'NONE', #28546, .T. ) ;
#31481=ORIENTED_EDGE ( 'NONE', *, *, #3606, .F. ) ;
#31529=CARTESIAN_POINT ( 'NONE',  ( 0.1085714285714300953, -3.798448662927791819, -0.7999999999999951594 ) ) ;
#31556=VECTOR ( 'NONE', #26371, 1000.000000000000000 ) ;
#31626=VERTEX_POINT ( 'NONE', #15220 ) ;
#31673=EDGE_CURVE ( 'NONE', #21688, #20267, #13345, .T. ) ;
#31695=ORIENTED_EDGE ( 'NONE', *, *, #19460, .F. ) ;
#31699=ADVANCED_FACE ( 'NONE', ( #31455 ), #6594, .F. ) ;
#31825=ORIENTED_EDGE ( 'NONE', *, *, #20955, .F. ) ;
#31920=ORIENTED_EDGE ( 'NONE', *, *, #16562, .F. ) ;
#31946=DIRECTION ( 'NONE',  ( 1.000000000000000000, -4.528031003192420052E-15, -1.174092375852883160E-15 ) ) ;
#31967=EDGE_CURVE ( 'NONE', #21828, #24050, #27664, .T. ) ;
#31991=DIRECTION ( 'NONE',  ( 0.02857142857142376188, 0.9995917534020517525, 3.884870526907702978E-16 ) ) ;
#32015=ADVANCED_FACE ( 'NONE', ( #626 ), #30178, .F. ) ;
#32035=VECTOR ( 'NONE', #15723, 1000.000000000000000 ) ;
#32114=ORIENTED_EDGE ( 'NONE', *, *, #27311, .F. ) ;
#32175=CARTESIAN_POINT ( 'NONE',  ( -2.321707774797454604, -4.824281976789094095, 0.000000000000000000 ) ) ;
#32235=ORIENTED_EDGE ( 'NONE', *, *, #18685, .F. ) ;
#32272=DIRECTION ( 'NONE',  ( 1.174092375852890457E-15, -4.222049128630259891E-16, -1.000000000000000000 ) ) ;
#32320=COLOUR_RGB ( '', 0.72549020, 0.75294118, 0.79215686) ;
#32323=DIRECTION ( 'NONE',  ( -1.174092375852890260E-15, 4.222049128630259891E-16, 1.000000000000000000 ) ) ;
#32362=CARTESIAN_POINT ( 'NONE',  ( 0.9999999999999453770, -6.008326913195871199, 0.000000000000000000 ) ) ;
#32423=DIRECTION ( 'NONE',  ( -1.174092375852890260E-15, 4.222049128630259891E-16, 1.000000000000000000 ) ) ;
#32448=LINE ( 'NONE', #7956, #5179 ) ;
#32493=VECTOR ( 'NONE', #1197, 1000.000000000000000 ) ;
#32518=AXIS2_PLACEMENT_3D ( 'NONE', #24586, #19336, #19511 ) ;
#32532=DIRECTION ( 'NONE',  ( 1.174092375852885330E-15, 4.222049128630153888E-16, 1.000000000000000000 ) ) ;
#32545=AXIS2_PLACEMENT_3D ( 'NONE', #3802, #14760, #3988 ) ;
#32556=ORIENTED_EDGE ( 'NONE', *, *, #13449, .F. ) ;
#32596=DIRECTION ( 'NONE',  ( 1.000000000000000000, -4.336808689941997226E-15, -1.084202172485499306E-15 ) ) ;
#32626=VERTEX_POINT ( 'NONE', #20846 ) ;
#32840=EDGE_CURVE ( 'NONE', #24139, #15081, #24729, .T. ) ;
#32897=CARTESIAN_POINT ( 'NONE',  ( -1.000000000000000888, -6.008326913195953800, -0.7999999999999951594 ) ) ;
#32939=ORIENTED_EDGE ( 'NONE', *, *, #18922, .T. ) ;
#32941=LINE ( 'NONE', #8785, #13003 ) ;
#32982=VERTEX_POINT ( 'NONE', #30408 ) ;
#32983=ORIENTED_EDGE ( 'NONE', *, *, #938, .T. ) ;
#33075=EDGE_CURVE ( 'NONE', #18320, #30963, #27536, .T. ) ;
#33080=CARTESIAN_POINT ( 'NONE',  ( 0.000000000000000000, 0.000000000000000000, 0.000000000000000000 ) ) ;
#33093=AXIS2_PLACEMENT_3D ( 'NONE', #4258, #15195, #25501 ) ;
#33147=VECTOR ( 'NONE', #15963, 1000.000000000000000 ) ;
#33283=EDGE_CURVE ( 'NONE', #32626, #27376, #1598, .T. ) ;
#33345=CIRCLE ( 'NONE', #31057, 0.7500000000000039968 ) ;
#33379=FACE_OUTER_BOUND ( 'NONE', #15788, .T. ) ;
#33444=AXIS2_PLACEMENT_3D ( 'NONE', #31272, #9836, #20439 ) ;
#33445=CARTESIAN_POINT ( 'NONE',  ( 0.1085714285714300953, -3.798448662927791819, 0.000000000000000000 ) ) ;
#33541=DIRECTION ( 'NONE',  ( -1.174092375852890260E-15, 4.222049128630259891E-16, 1.000000000000000000 ) ) ;
#33575=FACE_OUTER_BOUND ( 'NONE', #21292, .T. ) ;
#33677=EDGE_CURVE ( 'NONE', #16466, #22531, #19758, .T. ) ;
#33763=CARTESIAN_POINT ( 'NONE',  ( -1.000000000000014655, -5.408326913195881325, -0.7999999999999951594 ) ) ;
#33772=ORIENTED_EDGE ( 'NONE', *, *, #31967, .T. ) ;
#33782=CARTESIAN_POINT ( 'NONE',  ( 0.9999999999999453770, -6.008326913195871199, 0.000000000000000000 ) ) ;
#33820=AXIS2_PLACEMENT_3D ( 'NONE', #5374, #21542, #11121 ) ;
#33831=ORIENTED_EDGE ( 'NONE', *, *, #12631, .F. ) ;
#33833=CARTESIAN_POINT ( 'NONE',  ( -1.387778780781445676E-14, 0.4273491293403097746, 0.000000000000000000 ) ) ;
#33900=ADVANCED_FACE ( 'NONE', ( #3962 ), #26089, .F. ) ;
#33957=CARTESIAN_POINT ( 'NONE',  ( 3.160591952521676795, -3.281206521718066149, 0.000000000000000000 ) ) ;
#33996=LINE ( 'NONE', #9322, #28396 ) ;
#34031=EDGE_LOOP ( 'NONE', ( #33831, #29952, #18297, #6817 ) ) ;
#34058=STYLED_ITEM ( 'NONE', ( #11066 ), #22718 ) ;
#34064=EDGE_CURVE ( 'NONE', #34789, #7837, #7958, .T. ) ;
#34091=DIRECTION ( 'NONE',  ( 1.000000000000000000, -4.528031003192420052E-15, -1.179290629824070178E-15 ) ) ;
#34124=CARTESIAN_POINT ( 'NONE',  ( -1.387778780781445676E-14, 0.4273491293403097746, 0.000000000000000000 ) ) ;
#34221=CIRCLE ( 'NONE', #33093, 3.800000000000018918 ) ;
#34332=AXIS2_PLACEMENT_3D ( 'NONE', #11995, #28027, #9459 ) ;
#34338=AXIS2_PLACEMENT_3D ( 'NONE', #12088, #9206, #25608 ) ;
#34399=PLANE ( 'NONE',  #35093 ) ;
#34478=LINE ( 'NONE', #21127, #31556 ) ;
#34555=EDGE_LOOP ( 'NONE', ( #31920, #32235, #8856, #25565 ) ) ;
#34561=EDGE_CURVE ( 'NONE', #15465, #20170, #13013, .T. ) ;
#34602=CARTESIAN_POINT ( 'NONE',  ( 0.9999999999999870104, -5.408326913195881325, -0.7999999999999951594 ) ) ;
#34641=CYLINDRICAL_SURFACE ( 'NONE', #6109, 0.7500000000000041078 ) ;
#34652=VERTEX_POINT ( 'NONE', #26173 ) ;
#34701=DIRECTION ( 'NONE',  ( -1.174092375852890260E-15, 4.222049128630259891E-16, 1.000000000000000000 ) ) ;
#34707=ADVANCED_FACE ( 'NONE', ( #20206 ), #34641, .T. ) ;
#34733=CIRCLE ( 'NONE', #8375, 0.6000000000000028644 ) ;
#34788=ORIENTED_EDGE ( 'NONE', *, *, #25596, .F. ) ;
#34789=VERTEX_POINT ( 'NONE', #5288 ) ;
#34835=AXIS2_PLACEMENT_3D ( 'NONE', #2361, #3230, #19581 ) ;
#34942=CARTESIAN_POINT ( 'NONE',  ( 4.747884751462025044, -5.143694235356003119, -0.7999999999999951594 ) ) ;
#34954=EDGE_LOOP ( 'NONE', ( #9570, #7128, #23893, #17067 ) ) ;
#34989=AXIS2_PLACEMENT_3D ( 'NONE', #12942, #21382, #27167 ) ;
#35065=AXIS2_PLACEMENT_3D ( 'NONE', #26419, #10025, #31991 ) ;
#35084=LINE ( 'NONE', #10407, #285 ) ;
#35093=AXIS2_PLACEMENT_3D ( 'NONE', #9716, #15453, #4329 ) ;
#35101=ADVANCED_FACE ( 'NONE', ( #18011 ), #17663, .T. ) ;
#35103=CYLINDRICAL_SURFACE ( 'NONE', #34989, 4.872650870659778199 ) ;
#35124=EDGE_CURVE ( 'NONE', #35493, #10728, #4010, .T. ) ;
#35133=EDGE_LOOP ( 'NONE', ( #25696, #27483, #10211, #30981 ) ) ;
#35208=LINE ( 'NONE', #30335, #28586 ) ;
#35264=EDGE_CURVE ( 'NONE', #21428, #22807, #2014, .T. ) ;
#35331=ORIENTED_EDGE ( 'NONE', *, *, #30394, .F. ) ;
#35365=ADVANCED_FACE ( 'NONE', ( #10639 ), #21595, .F. ) ;
#35399=ORIENTED_EDGE ( 'NONE', *, *, #25362, .F. ) ;
#35450=SHAPE_DEFINITION_REPRESENTATION ( #25315, #2005 ) ;
#35493=VERTEX_POINT ( 'NONE', #19081 ) ;
#35516=DIRECTION ( 'NONE',  ( 1.000000000000000000, -4.336808689941997226E-15, -1.084202172485499306E-15 ) ) ;
#35593=CARTESIAN_POINT ( 'NONE',  ( 0.000000000000000000, 0.000000000000000000, -0.7999999999999951594 ) ) ;
ENDSEC;
END-ISO-10303-21;
